ISO-10303-21;
HEADER;
FILE_DESCRIPTION (('STEP AP214'),
    '1' );
FILE_NAME ('Top Mounting Plate.step',
    '2026-10-09T12:05:53',
    ( '' ),
    ( '' ),
    'SwSTEP 2.0',
    'SolidWorks 2026',
    '' );
FILE_SCHEMA (( 'AUTOMOTIVE_DESIGN' ));
ENDSEC;

DATA;
#18=SHAPE_DEFINITION_REPRESENTATION ( #45804, #4374 ) ;
#36=DIRECTION ( 'NONE',  ( 0.5877852522924696954, 0.8090169943749498938, 0.000000000000000000 ) ) ;
#38=AXIS2_PLACEMENT_3D ( 'NONE', #21905, #42103, #29767 ) ;
#51=CYLINDRICAL_SURFACE ( 'NONE', #25451, 0.9999999999999988898 ) ;
#52=AXIS2_PLACEMENT_3D ( 'NONE', #15855, #20801, #24196 ) ;
#62=AXIS2_PLACEMENT_3D ( 'NONE', #47458, #35380, #23303 ) ;
#79=CARTESIAN_POINT ( 'NONE',  ( 53.63393739769619373, -53.11618894467930119, 16.35000000000000142 ) ) ;
#87=AXIS2_PLACEMENT_3D ( 'NONE', #9634, #13072, #16715 ) ;
#110=EDGE_CURVE ( 'NONE', #14338, #30215, #34341, .T. ) ;
#132=DIRECTION ( 'NONE',  ( 0.000000000000000000, 0.000000000000000000, -1.000000000000000000 ) ) ;
#159=CARTESIAN_POINT ( 'NONE',  ( -14.41646913324137458, -47.38337005707102634, 16.85000000000000142 ) ) ;
#163=EDGE_CURVE ( 'NONE', #42293, #16351, #20947, .T. ) ;
#176=ORIENTED_EDGE ( 'NONE', *, *, #14775, .F. ) ;
#188=EDGE_CURVE ( 'NONE', #6898, #18473, #14502, .T. ) ;
#208=DIRECTION ( 'NONE',  ( 1.000000000000000000, 0.000000000000000000, 0.000000000000000000 ) ) ;
#219=AXIS2_PLACEMENT_3D ( 'NONE', #32252, #16823, #17087 ) ;
#224=LINE ( 'NONE', #43991, #1797 ) ;
#235=VERTEX_POINT ( 'NONE', #24656 ) ;
#244=CARTESIAN_POINT ( 'NONE',  ( -18.86606260230360022, -50.61618894467959962, 17.35000000000000142 ) ) ;
#245=AXIS2_PLACEMENT_3D ( 'NONE', #20946, #48226, #25130 ) ;
#255=DIRECTION ( 'NONE',  ( 0.000000000000000000, 0.000000000000000000, -1.000000000000000000 ) ) ;
#268=EDGE_CURVE ( 'NONE', #31144, #33328, #44340, .T. ) ;
#297=AXIS2_PLACEMENT_3D ( 'NONE', #33472, #4412, #32417 ) ;
#303=CYLINDRICAL_SURFACE ( 'NONE', #11626, 0.9999999999999988898 ) ;
#310=DIRECTION ( 'NONE',  ( 1.224645063448482957E-16, 1.000000000000000000, -1.376914871200490233E-11 ) ) ;
#339=FACE_OUTER_BOUND ( 'NONE', #8165, .T. ) ;
#340=CARTESIAN_POINT ( 'NONE',  ( 2.633937397696199501, -15.61618894467929763, -1.149999999999999911 ) ) ;
#342=ORIENTED_EDGE ( 'NONE', *, *, #163, .T. ) ;
#352=EDGE_CURVE ( 'NONE', #42477, #4597, #41871, .T. ) ;
#371=VERTEX_POINT ( 'NONE', #34078 ) ;
#398=CARTESIAN_POINT ( 'NONE',  ( 22.23393739769620225, -15.61618894467929941, -8.849999999999999645 ) ) ;
#410=ORIENTED_EDGE ( 'NONE', *, *, #13192, .T. ) ;
#426=ORIENTED_EDGE ( 'NONE', *, *, #33634, .T. ) ;
#434=VERTEX_POINT ( 'NONE', #14181 ) ;
#449=DIRECTION ( 'NONE',  ( 0.000000000000000000, 0.000000000000000000, 1.000000000000000000 ) ) ;
#451=FACE_OUTER_BOUND ( 'NONE', #25206, .T. ) ;
#452=EDGE_CURVE ( 'NONE', #19246, #15767, #46171, .T. ) ;
#482=DIRECTION ( 'NONE',  ( 1.000000000000000000, -1.080128361472376380E-29, -1.260570937617230037E-11 ) ) ;
#487=CARTESIAN_POINT ( 'NONE',  ( -31.36606260230380272, -53.11618894467930119, 11.84999999999999964 ) ) ;
#495=TOROIDAL_SURFACE ( 'NONE', #15595, 9.000000000000000000, 1.000000000000000000 ) ;
#507=CARTESIAN_POINT ( 'NONE',  ( -21.36606260230379917, -53.11618894467930119, 10.84999999999999964 ) ) ;
#512=ADVANCED_FACE ( 'NONE', ( #1871 ), #3388, .F. ) ;
#526=AXIS2_PLACEMENT_3D ( 'NONE', #41480, #49623, #33347 ) ;
#563=CARTESIAN_POINT ( 'NONE',  ( 33.77213399851893172, -15.61618894397937929, 14.62639320225000006 ) ) ;
#631=DIRECTION ( 'NONE',  ( 0.000000000000000000, -1.000000000000000000, 0.000000000000000000 ) ) ;
#642=AXIS2_PLACEMENT_3D ( 'NONE', #26175, #25655, #45863 ) ;
#647=CARTESIAN_POINT ( 'NONE',  ( -3.175079596678700433, -15.61618894467929941, 17.35000000000000142 ) ) ;
#687=ORIENTED_EDGE ( 'NONE', *, *, #17798, .F. ) ;
#693=DIRECTION ( 'NONE',  ( 0.000000000000000000, 1.000000000000000000, 0.000000000000000000 ) ) ;
#704=EDGE_CURVE ( 'NONE', #47505, #49517, #4236, .T. ) ;
#708=DIRECTION ( 'NONE',  ( 0.000000000000000000, 0.000000000000000000, 1.000000000000000000 ) ) ;
#720=DIRECTION ( 'NONE',  ( 0.000000000000000000, -1.000000000000000000, 0.000000000000000000 ) ) ;
#725=EDGE_LOOP ( 'NONE', ( #14856, #9355, #28472, #46085, #1468 ) ) ;
#727=VERTEX_POINT ( 'NONE', #23818 ) ;
#728=LINE ( 'NONE', #25080, #19485 ) ;
#767=ORIENTED_EDGE ( 'NONE', *, *, #26058, .T. ) ;
#789=CARTESIAN_POINT ( 'NONE',  ( 52.63393739706710051, -15.61618894417471104, 10.85000000030205669 ) ) ;
#799=EDGE_CURVE ( 'NONE', #15443, #35304, #28536, .T. ) ;
#824=VECTOR ( 'NONE', #36277, 1000.000000000000000 ) ;
#826=DIRECTION ( 'NONE',  ( 1.430038757655089944E-15, 8.684364315601310195E-16, -1.000000000000000000 ) ) ;
#836=EDGE_CURVE ( 'NONE', #26710, #12957, #17026, .T. ) ;
#878=DIRECTION ( 'NONE',  ( 0.000000000000000000, 1.000000000000000000, 0.000000000000000000 ) ) ;
#881=DIRECTION ( 'NONE',  ( -1.000000000000000000, 0.000000000000000000, 0.000000000000000000 ) ) ;
#886=ORIENTED_EDGE ( 'NONE', *, *, #11704, .T. ) ;
#889=CARTESIAN_POINT ( 'NONE',  ( 63.63393739769619373, 31.88381105532059934, 17.35000000000000142 ) ) ;
#895=CARTESIAN_POINT ( 'NONE',  ( -28.43713041416928178, -60.18725675654477669, 17.35000000000000142 ) ) ;
#900=PRODUCT_DEFINITION_FORMATION_WITH_SPECIFIED_SOURCE ( 'ANY', '', #35664, .NOT_KNOWN. ) ;
#929=CARTESIAN_POINT ( 'NONE',  ( -21.36606260230379917, -63.11618894467929408, 16.35000000000000142 ) ) ;
#1029=ORIENTED_EDGE ( 'NONE', *, *, #45351, .T. ) ;
#1049=AXIS2_PLACEMENT_3D ( 'NONE', #35049, #51057, #39260 ) ;
#1052=DIRECTION ( 'NONE',  ( 1.000000000000000000, 0.000000000000000000, 0.000000000000000000 ) ) ;
#1082=VERTEX_POINT ( 'NONE', #15414 ) ;
#1099=ORIENTED_EDGE ( 'NONE', *, *, #24455, .T. ) ;
#1102=CARTESIAN_POINT ( 'NONE',  ( 16.13393739769620083, -15.61618894467929941, -9.721247897589949005 ) ) ;
#1103=AXIS2_PLACEMENT_3D ( 'NONE', #43812, #16805, #7910 ) ;
#1112=ORIENTED_EDGE ( 'NONE', *, *, #13564, .T. ) ;
#1118=AXIS2_PLACEMENT_3D ( 'NONE', #6228, #14083, #30044 ) ;
#1128=CARTESIAN_POINT ( 'NONE',  ( 53.63393739769619373, -62.11618894467930119, 11.84999999999999964 ) ) ;
#1144=EDGE_LOOP ( 'NONE', ( #12960, #15336, #21444, #25660, #40732 ) ) ;
#1234=CIRCLE ( 'NONE', #12959, 9.768249999999998323 ) ;
#1275=DIRECTION ( 'NONE',  ( -0.5720614028176828070, 0.4156269377774549079, -0.7071067811865477948 ) ) ;
#1350=VERTEX_POINT ( 'NONE', #10501 ) ;
#1389=CARTESIAN_POINT ( 'NONE',  ( -28.43713041416927467, 28.95487886718607129, 16.35000000000000142 ) ) ;
#1397=ORIENTED_EDGE ( 'NONE', *, *, #19551, .F. ) ;
#1404=CIRCLE ( 'NONE', #14796, 13.50000000000000178 ) ;
#1405=ORIENTED_EDGE ( 'NONE', *, *, #32872, .F. ) ;
#1416=DIRECTION ( 'NONE',  ( 0.000000000000000000, 0.000000000000000000, 1.000000000000000000 ) ) ;
#1419=ORIENTED_EDGE ( 'NONE', *, *, #15135, .F. ) ;
#1424=ORIENTED_EDGE ( 'NONE', *, *, #38832, .F. ) ;
#1439=ORIENTED_EDGE ( 'NONE', *, *, #19864, .T. ) ;
#1465=ORIENTED_EDGE ( 'NONE', *, *, #26717, .T. ) ;
#1468=ORIENTED_EDGE ( 'NONE', *, *, #29771, .T. ) ;
#1472=CARTESIAN_POINT ( 'NONE',  ( 53.63393739769619373, 31.59091783650714547, 11.14289321881345174 ) ) ;
#1474=AXIS2_PLACEMENT_3D ( 'NONE', #20240, #40428, #9254 ) ;
#1492=DIRECTION ( 'NONE',  ( 0.000000000000000000, -3.858025010473989332E-12, -1.000000000000000000 ) ) ;
#1531=ADVANCED_FACE ( 'NONE', ( #37690 ), #21940, .T. ) ;
#1543=EDGE_LOOP ( 'NONE', ( #23972, #20280, #24064, #34922 ) ) ;
#1544=CARTESIAN_POINT ( 'NONE',  ( 62.63393739769619373, -53.11618894467930119, 16.35000000000000142 ) ) ;
#1547=CIRCLE ( 'NONE', #33326, 10.00000000000000355 ) ;
#1568=EDGE_CURVE ( 'NONE', #38311, #20782, #37722, .T. ) ;
#1583=VECTOR ( 'NONE', #1605, 1000.000000000000114 ) ;
#1605=DIRECTION ( 'NONE',  ( -0.4156269377774524099, -0.5720614028176843613, -0.7071067811865480168 ) ) ;
#1617=ORIENTED_EDGE ( 'NONE', *, *, #45206, .F. ) ;
#1624=CIRCLE ( 'NONE', #10003, 1.000000000000000888 ) ;
#1654=AXIS2_PLACEMENT_3D ( 'NONE', #2847, #31113, #42939 ) ;
#1699=ADVANCED_FACE ( 'NONE', ( #47625 ), #46868, .F. ) ;
#1704=CARTESIAN_POINT ( 'NONE',  ( -24.36606260230359666, -50.61618894467959962, 11.34999999999999964 ) ) ;
#1711=AXIS2_PLACEMENT_3D ( 'NONE', #40553, #24278, #48686 ) ;
#1712=ORIENTED_EDGE ( 'NONE', *, *, #3770, .F. ) ;
#1725=ORIENTED_EDGE ( 'NONE', *, *, #8148, .T. ) ;
#1755=CARTESIAN_POINT ( 'NONE',  ( -13.36606260230359844, -50.61618894467959962, 14.21249999999999858 ) ) ;
#1756=FACE_OUTER_BOUND ( 'NONE', #35636, .T. ) ;
#1760=AXIS2_PLACEMENT_3D ( 'NONE', #42868, #3025, #27121 ) ;
#1773=DIRECTION ( 'NONE',  ( 0.000000000000000000, 0.000000000000000000, -1.000000000000000000 ) ) ;
#1782=VERTEX_POINT ( 'NONE', #3484 ) ;
#1797=VECTOR ( 'NONE', #24040, 1000.000000000000000 ) ;
#1801=DIRECTION ( 'NONE',  ( 0.000000000000000000, -1.000000000000000000, 0.000000000000000000 ) ) ;
#1817=ORIENTED_EDGE ( 'NONE', *, *, #5322, .F. ) ;
#1824=DIRECTION ( 'NONE',  ( 0.8090169943749525583, 0.5877852522924661427, 0.000000000000000000 ) ) ;
#1857=CARTESIAN_POINT ( 'NONE',  ( 39.88393739769619373, 31.59091783650714547, 17.05710678118654755 ) ) ;
#1864=ORIENTED_EDGE ( 'NONE', *, *, #31561, .F. ) ;
#1866=DIRECTION ( 'NONE',  ( 1.000000000000000000, 0.000000000000000000, 0.000000000000000000 ) ) ;
#1871=FACE_OUTER_BOUND ( 'NONE', #2040, .T. ) ;
#1887=CYLINDRICAL_SURFACE ( 'NONE', #44089, 1.000000000000003775 ) ;
#1900=VERTEX_POINT ( 'NONE', #21242 ) ;
#1938=AXIS2_PLACEMENT_3D ( 'NONE', #45067, #36160, #20420 ) ;
#1971=EDGE_LOOP ( 'NONE', ( #47071, #17443, #38687, #7155, #20399 ) ) ;
#1989=CIRCLE ( 'NONE', #1118, 5.499999999999998224 ) ;
#2040=EDGE_LOOP ( 'NONE', ( #5607, #38553, #13786, #44927, #10429 ) ) ;
#2082=ADVANCED_FACE ( 'NONE', ( #21505 ), #11019, .F. ) ;
#2087=VECTOR ( 'NONE', #47340, 1000.000000000000000 ) ;
#2089=CARTESIAN_POINT ( 'NONE',  ( 51.13393739769620083, 19.38381105532069881, 11.34999999999999964 ) ) ;
#2095=ORIENTED_EDGE ( 'NONE', *, *, #33459, .F. ) ;
#2118=VERTEX_POINT ( 'NONE', #10768 ) ;
#2120=CARTESIAN_POINT ( 'NONE',  ( 16.13393739769620083, -15.61618894467929941, -1.149999999999999911 ) ) ;
#2131=FACE_BOUND ( 'NONE', #44388, .T. ) ;
#2136=CYLINDRICAL_SURFACE ( 'NONE', #31309, 1.000000000000001332 ) ;
#2141=EDGE_CURVE ( 'NONE', #8577, #47254, #46985, .T. ) ;
#2164=CARTESIAN_POINT ( 'NONE',  ( 16.13393739769620083, -15.61618894467929941, -12.13039854958090125 ) ) ;
#2168=DIRECTION ( 'NONE',  ( 0.000000000000000000, 0.000000000000000000, -1.000000000000000000 ) ) ;
#2180=AXIS2_PLACEMENT_3D ( 'NONE', #11320, #51407, #3711 ) ;
#2195=DIRECTION ( 'NONE',  ( 0.000000000000000000, -1.000000000000000000, 0.000000000000000000 ) ) ;
#2196=AXIS2_PLACEMENT_3D ( 'NONE', #50565, #2611, #14655 ) ;
#2214=AXIS2_PLACEMENT_3D ( 'NONE', #10095, #29476, #45221 ) ;
#2221=CONICAL_SURFACE ( 'NONE', #31492, 0.6299999999999942313, 0.7853981633974476129 ) ;
#2226=CARTESIAN_POINT ( 'NONE',  ( 34.13393739769620083, -15.61618894467929941, -18.58999999999999986 ) ) ;
#2239=DIRECTION ( 'NONE',  ( 0.000000000000000000, 0.000000000000000000, -1.000000000000000000 ) ) ;
#2252=EDGE_LOOP ( 'NONE', ( #37375, #21111 ) ) ;
#2273=AXIS2_PLACEMENT_3D ( 'NONE', #10654, #41579, #30021 ) ;
#2296=DIRECTION ( 'NONE',  ( 1.062456999999999985E-16, -7.719205000000000365E-17, 1.000000000000000000 ) ) ;
#2307=ORIENTED_EDGE ( 'NONE', *, *, #27466, .F. ) ;
#2317=ORIENTED_EDGE ( 'NONE', *, *, #20342, .F. ) ;
#2330=AXIS2_PLACEMENT_3D ( 'NONE', #28657, #28400, #20275 ) ;
#2338=CARTESIAN_POINT ( 'NONE',  ( 53.63393739769619373, -63.11618894467929408, 16.35000000000000142 ) ) ;
#2339=CARTESIAN_POINT ( 'NONE',  ( 51.50424210664085223, -51.12586965113519710, 11.97999999999999865 ) ) ;
#2343=DIRECTION ( 'NONE',  ( 0.000000000000000000, 0.000000000000000000, 1.000000000000000000 ) ) ;
#2351=DIRECTION ( 'NONE',  ( 0.000000000000000000, 0.000000000000000000, -1.000000000000000000 ) ) ;
#2354=CARTESIAN_POINT ( 'NONE',  ( 51.13393739769620083, 19.38381105532069881, 11.97999999999999865 ) ) ;
#2380=ORIENTED_EDGE ( 'NONE', *, *, #19648, .F. ) ;
#2384=DIRECTION ( 'NONE',  ( 0.000000000000000000, -9.718338800990680596E-16, 1.000000000000000000 ) ) ;
#2413=DIRECTION ( 'NONE',  ( 0.4156269377774536866, -0.5720614028176834731, 0.7071067811865480168 ) ) ;
#2418=DIRECTION ( 'NONE',  ( 0.000000000000000000, -1.000000000000000000, 0.000000000000000000 ) ) ;
#2443=CARTESIAN_POINT ( 'NONE',  ( -31.36606260230380272, -63.11618894467929408, 10.84999999999999964 ) ) ;
#2444=TOROIDAL_SURFACE ( 'NONE', #24181, 17.07000000028409659, 3.569999999987189643 ) ;
#2448=CIRCLE ( 'NONE', #15836, 10.00000000000000711 ) ;
#2460=FACE_OUTER_BOUND ( 'NONE', #41298, .T. ) ;
#2468=DIRECTION ( 'NONE',  ( 0.000000000000000000, 0.000000000000000000, -1.000000000000000000 ) ) ;
#2501=ORIENTED_EDGE ( 'NONE', *, *, #42022, .T. ) ;
#2503=ORIENTED_EDGE ( 'NONE', *, *, #16917, .T. ) ;
#2510=CYLINDRICAL_SURFACE ( 'NONE', #20187, 5.499999999999998224 ) ;
#2512=AXIS2_PLACEMENT_3D ( 'NONE', #34984, #39708, #23432 ) ;
#2534=ORIENTED_EDGE ( 'NONE', *, *, #34724, .T. ) ;
#2538=DIRECTION ( 'NONE',  ( 1.000000000000000000, 0.000000000000000000, 0.000000000000000000 ) ) ;
#2546=AXIS2_PLACEMENT_3D ( 'NONE', #48343, #132, #24721 ) ;
#2581=ORIENTED_EDGE ( 'NONE', *, *, #30396, .F. ) ;
#2607=DIRECTION ( 'NONE',  ( 1.000000000000000000, -1.080128361472376380E-29, -1.260570937617230037E-11 ) ) ;
#2611=DIRECTION ( 'NONE',  ( 4.718060457820110146E-11, -8.281540456132319756E-12, 1.000000000000000000 ) ) ;
#2617=ORIENTED_EDGE ( 'NONE', *, *, #37878, .F. ) ;
#2653=LINE ( 'NONE', #41698, #21680 ) ;
#2657=EDGE_CURVE ( 'NONE', #18765, #29187, #24260, .T. ) ;
#2660=ORIENTED_EDGE ( 'NONE', *, *, #42944, .F. ) ;
#2665=DIRECTION ( 'NONE',  ( 1.224647809895004774E-16, 1.000000000000000000, -3.858400438143726299E-12 ) ) ;
#2668=CIRCLE ( 'NONE', #5183, 4.649999999999999467 ) ;
#2685=CARTESIAN_POINT ( 'NONE',  ( -23.72016456855330091, -54.14290045843440424, 17.35000000000000142 ) ) ;
#2689=FACE_OUTER_BOUND ( 'NONE', #26055, .T. ) ;
#2702=VERTEX_POINT ( 'NONE', #5168 ) ;
#2719=LINE ( 'NONE', #39394, #13757 ) ;
#2733=EDGE_LOOP ( 'NONE', ( #29216, #33986, #12183, #24840, #4810 ) ) ;
#2756=CARTESIAN_POINT ( 'NONE',  ( 2.633937397696199945, -15.61618894467930119, 17.35000000000000142 ) ) ;
#2787=CARTESIAN_POINT ( 'NONE',  ( 5.133937397696200833, -15.61618894467929763, -20.58999999999999986 ) ) ;
#2795=CIRCLE ( 'NONE', #51356, 20.00000000000000000 ) ;
#2847=CARTESIAN_POINT ( 'NONE',  ( -31.36606260230380272, -63.11618894467929408, 17.35000000000000142 ) ) ;
#2854=LINE ( 'NONE', #35588, #3344 ) ;
#2881=DIRECTION ( 'NONE',  ( 0.7071067811865473507, 0.7071067811865476838, 0.000000000000000000 ) ) ;
#2885=DIRECTION ( 'NONE',  ( -1.000000000000000000, 0.000000000000000000, 0.000000000000000000 ) ) ;
#2886=ADVANCED_FACE ( 'NONE', ( #41310 ), #21058, .F. ) ;
#2887=ORIENTED_EDGE ( 'NONE', *, *, #50559, .F. ) ;
#2888=AXIS2_PLACEMENT_3D ( 'NONE', #14526, #2468, #39416 ) ;
#2914=AXIS2_PLACEMENT_3D ( 'NONE', #17919, #50155, #13743 ) ;
#2955=CARTESIAN_POINT ( 'NONE',  ( -21.36606260230379917, 21.88381105532059934, 16.35000000000000142 ) ) ;
#2958=EDGE_LOOP ( 'NONE', ( #3950, #45172, #15913, #20138 ) ) ;
#3004=DIRECTION ( 'NONE',  ( 0.000000000000000000, 0.000000000000000000, -1.000000000000000000 ) ) ;
#3025=DIRECTION ( 'NONE',  ( 0.000000000000000000, 0.000000000000000000, 1.000000000000000000 ) ) ;
#3032=DIRECTION ( 'NONE',  ( -1.000000000000000000, 0.000000000000000000, 0.000000000000000000 ) ) ;
#3068=VERTEX_POINT ( 'NONE', #1389 ) ;
#3075=VECTOR ( 'NONE', #10209, 999.9999999999998863 ) ;
#3081=EDGE_CURVE ( 'NONE', #32578, #45801, #8506, .T. ) ;
#3090=DIRECTION ( 'NONE',  ( 0.000000000000000000, 0.000000000000000000, 1.000000000000000000 ) ) ;
#3135=EDGE_CURVE ( 'NONE', #7519, #50005, #39973, .T. ) ;
#3175=VERTEX_POINT ( 'NONE', #37541 ) ;
#3184=DIRECTION ( 'NONE',  ( 0.000000000000000000, 0.000000000000000000, -1.000000000000000000 ) ) ;
#3199=DIRECTION ( 'NONE',  ( 0.000000000000000000, 0.000000000000000000, -1.000000000000000000 ) ) ;
#3222=ORIENTED_EDGE ( 'NONE', *, *, #8942, .T. ) ;
#3240=CIRCLE ( 'NONE', #28344, 6.100000000000001421 ) ;
#3241=CIRCLE ( 'NONE', #30110, 5.499999999999998224 ) ;
#3253=CARTESIAN_POINT ( 'NONE',  ( 54.36675628530516491, -46.16659547561676646, 11.34999999999999964 ) ) ;
#3271=DIRECTION ( 'NONE',  ( 0.7071067811865475727, -0.7071067811865475727, 0.000000000000000000 ) ) ;
#3289=EDGE_LOOP ( 'NONE', ( #27738, #42439, #25974, #5934, #12896, #19451, #33209 ) ) ;
#3302=CARTESIAN_POINT ( 'NONE',  ( -31.36606260230380272, 21.88381105532059934, 16.35000000000000142 ) ) ;
#3303=CIRCLE ( 'NONE', #12509, 9.768249999999998323 ) ;
#3309=CONICAL_SURFACE ( 'NONE', #30936, 0.6299999999999942313, 0.7853981633974476129 ) ;
#3317=CARTESIAN_POINT ( 'NONE',  ( 16.13393739769620083, -15.61618894467929941, -19.83999999999999986 ) ) ;
#3326=ORIENTED_EDGE ( 'NONE', *, *, #1568, .F. ) ;
#3328=DIRECTION ( 'NONE',  ( 1.000000000000000000, 0.000000000000000000, 0.000000000000000000 ) ) ;
#3333=DIRECTION ( 'NONE',  ( 0.000000000000000000, 8.281569874363147012E-12, -1.000000000000000000 ) ) ;
#3344=VECTOR ( 'NONE', #27194, 1000.000000000000000 ) ;
#3372=DIRECTION ( 'NONE',  ( 0.000000000000000000, 0.000000000000000000, 1.000000000000000000 ) ) ;
#3381=CARTESIAN_POINT ( 'NONE',  ( 34.63393739830264906, -15.61618894523020806, 9.349999999709213583 ) ) ;
#3388=CONICAL_SURFACE ( 'NONE', #62, 1.079032500000002059, 0.7853981633974469467 ) ;
#3435=ORIENTED_EDGE ( 'NONE', *, *, #44316, .T. ) ;
#3477=EDGE_CURVE ( 'NONE', #13741, #41355, #8180, .T. ) ;
#3480=ORIENTED_EDGE ( 'NONE', *, *, #42206, .F. ) ;
#3484=CARTESIAN_POINT ( 'NONE',  ( 1.864336597259699468, -25.98366078385575761, 14.62639320225000006 ) ) ;
#3485=ORIENTED_EDGE ( 'NONE', *, *, #25888, .T. ) ;
#3488=ADVANCED_FACE ( 'NONE', ( #35997 ), #48321, .F. ) ;
#3500=AXIS2_PLACEMENT_3D ( 'NONE', #30825, #46853, #10941 ) ;
#3504=CIRCLE ( 'NONE', #36960, 13.00000000000000178 ) ;
#3512=ORIENTED_EDGE ( 'NONE', *, *, #17381, .F. ) ;
#3531=VECTOR ( 'NONE', #19258, 1000.000000000000000 ) ;
#3534=CARTESIAN_POINT ( 'NONE',  ( 53.63393739769619373, -62.11618894467930119, 11.84999999999999964 ) ) ;
#3536=DIRECTION ( 'NONE',  ( 0.000000000000000000, 1.205285871143275290E-11, 1.000000000000000000 ) ) ;
#3542=EDGE_LOOP ( 'NONE', ( #2317, #36067, #29860, #17462, #34941, #27374 ) ) ;
#3545=ORIENTED_EDGE ( 'NONE', *, *, #42948, .T. ) ;
#3563=FACE_OUTER_BOUND ( 'NONE', #32081, .T. ) ;
#3565=AXIS2_PLACEMENT_3D ( 'NONE', #21246, #37255, #33309 ) ;
#3588=EDGE_LOOP ( 'NONE', ( #49351, #47072, #10285, #4049 ) ) ;
#3608=EDGE_LOOP ( 'NONE', ( #47559, #47230, #1424, #49345 ) ) ;
#3654=CARTESIAN_POINT ( 'NONE',  ( 53.63393739769619373, 30.88381105532059934, 11.84999999999999964 ) ) ;
#3655=CARTESIAN_POINT ( 'NONE',  ( 16.13393739769620083, -15.61618894467929941, -19.08999999999999986 ) ) ;
#3692=ORIENTED_EDGE ( 'NONE', *, *, #45795, .T. ) ;
#3696=DIRECTION ( 'NONE',  ( 0.000000000000000000, 0.000000000000000000, 1.000000000000000000 ) ) ;
#3711=DIRECTION ( 'NONE',  ( 0.5877852522924696954, 0.8090169943749498938, 0.000000000000000000 ) ) ;
#3716=DIRECTION ( 'NONE',  ( 0.000000000000000000, 0.000000000000000000, 1.000000000000000000 ) ) ;
#3751=AXIS2_PLACEMENT_3D ( 'NONE', #46899, #19353, #35601 ) ;
#3753=PLANE ( 'NONE',  #44725 ) ;
#3769=LINE ( 'NONE', #23387, #35574 ) ;
#3770=EDGE_CURVE ( 'NONE', #17150, #38311, #35485, .T. ) ;
#3794=CARTESIAN_POINT ( 'NONE',  ( -18.35638189584738456, -50.98649365362386021, 16.21999999999999886 ) ) ;
#3807=EDGE_LOOP ( 'NONE', ( #37932, #37044 ) ) ;
#3838=DIRECTION ( 'NONE',  ( 0.000000000000000000, 0.000000000000000000, -1.000000000000000000 ) ) ;
#3854=ORIENTED_EDGE ( 'NONE', *, *, #28869, .F. ) ;
#3861=CIRCLE ( 'NONE', #23906, 1.000000000000000888 ) ;
#3875=CARTESIAN_POINT ( 'NONE',  ( 62.63393739769619373, -53.11618894467930119, 11.84999999999999964 ) ) ;
#3890=ORIENTED_EDGE ( 'NONE', *, *, #14378, .F. ) ;
#3904=DIRECTION ( 'NONE',  ( 1.000000000000000000, 0.000000000000000000, 0.000000000000000000 ) ) ;
#3906=EDGE_CURVE ( 'NONE', #50052, #1350, #37032, .T. ) ;
#3913=CARTESIAN_POINT ( 'NONE',  ( -18.86606260230390220, 19.38381105532060289, 14.21249999999999858 ) ) ;
#3941=EDGE_LOOP ( 'NONE', ( #31296, #22311, #33123, #14822, #9849, #24848 ) ) ;
#3943=DIRECTION ( 'NONE',  ( 1.241897755690669394E-30, -1.000000000000000000, -8.684364315601310195E-16 ) ) ;
#3950=ORIENTED_EDGE ( 'NONE', *, *, #13564, .F. ) ;
#3992=ORIENTED_EDGE ( 'NONE', *, *, #14794, .F. ) ;
#4035=LINE ( 'NONE', #11646, #36771 ) ;
#4049=ORIENTED_EDGE ( 'NONE', *, *, #799, .F. ) ;
#4052=CARTESIAN_POINT ( 'NONE',  ( -22.39277411605872459, 14.52970908907091996, 10.84999999999999964 ) ) ;
#4105=AXIS2_PLACEMENT_3D ( 'NONE', #36156, #49009, #24337 ) ;
#4106=ORIENTED_EDGE ( 'NONE', *, *, #268, .F. ) ;
#4127=CARTESIAN_POINT ( 'NONE',  ( 16.13393739769620083, -15.61618894467929941, -5.690000000000000391 ) ) ;
#4137=CYLINDRICAL_SURFACE ( 'NONE', #14898, 20.00000000000000000 ) ;
#4161=DIRECTION ( 'NONE',  ( 0.000000000000000000, -1.000000000000000000, 0.000000000000000000 ) ) ;
#4180=ADVANCED_FACE ( 'NONE', ( #18148, #38328 ), #38598, .T. ) ;
#4188=DIRECTION ( 'NONE',  ( -1.000000000000000000, 0.000000000000000000, 0.000000000000000000 ) ) ;
#4191=VERTEX_POINT ( 'NONE', #26258 ) ;
#4198=ADVANCED_FACE ( 'NONE', ( #2689 ), #18661, .T. ) ;
#4201=DIRECTION ( 'NONE',  ( -1.000000000000000000, 0.000000000000000000, 0.000000000000000000 ) ) ;
#4236=CIRCLE ( 'NONE', #11813, 5.499999999999998224 ) ;
#4242=ADVANCED_FACE ( 'NONE', ( #50390 ), #49873, .T. ) ;
#4247=ORIENTED_EDGE ( 'NONE', *, *, #8942, .F. ) ;
#4252=FACE_OUTER_BOUND ( 'NONE', #47687, .T. ) ;
#4259=EDGE_CURVE ( 'NONE', #4597, #47505, #32483, .T. ) ;
#4271=CARTESIAN_POINT ( 'NONE',  ( 6.133937397696199945, -15.61618894467930119, -2.149999999999999911 ) ) ;
#4282=DIRECTION ( 'NONE',  ( 0.000000000000000000, 0.000000000000000000, 1.000000000000000000 ) ) ;
#4285=DIRECTION ( 'NONE',  ( 0.000000000000000000, -1.000000000000000000, 0.000000000000000000 ) ) ;
#4290=CYLINDRICAL_SURFACE ( 'NONE', #12513, 10.00000000000000355 ) ;
#4320=EDGE_CURVE ( 'NONE', #28785, #3175, #34218, .T. ) ;
#4343=ORIENTED_EDGE ( 'NONE', *, *, #8321, .F. ) ;
#4346=ORIENTED_EDGE ( 'NONE', *, *, #24452, .F. ) ;
#4371=DIRECTION ( 'NONE',  ( 0.000000000000000000, 0.000000000000000000, -1.000000000000000000 ) ) ;
#4373=AXIS2_PLACEMENT_3D ( 'NONE', #35818, #23480, #28194 ) ;
#4374=SHAPE_REPRESENTATION ( 'Top Mounting Plate', ( #20940 ), #40219 ) ;
#4395=CARTESIAN_POINT ( 'NONE',  ( 19.89586642153968299, -12.88298752151932014, -9.721247897589949005 ) ) ;
#4403=CARTESIAN_POINT ( 'NONE',  ( 53.63393739769619373, 30.88381105532059934, 16.35000000000000142 ) ) ;
#4412=DIRECTION ( 'NONE',  ( 0.000000000000000000, 0.000000000000000000, 1.000000000000000000 ) ) ;
#4461=AXIS2_PLACEMENT_3D ( 'NONE', #3913, #8610, #27741 ) ;
#4481=CIRCLE ( 'NONE', #297, 19.30901699437490038 ) ;
#4484=DIRECTION ( 'NONE',  ( 0.000000000000000000, -1.000000000000000000, 0.000000000000000000 ) ) ;
#4500=VERTEX_POINT ( 'NONE', #11972 ) ;
#4532=CARTESIAN_POINT ( 'NONE',  ( 51.13393739769620083, 19.38381105532069881, 10.84999999999999964 ) ) ;
#4536=CIRCLE ( 'NONE', #25476, 9.500000000000000000 ) ;
#4551=ORIENTED_EDGE ( 'NONE', *, *, #20681, .F. ) ;
#4554=EDGE_CURVE ( 'NONE', #17966, #12701, #23468, .T. ) ;
#4568=DIRECTION ( 'NONE',  ( 0.000000000000000000, 1.000000000000000000, 0.000000000000000000 ) ) ;
#4597=VERTEX_POINT ( 'NONE', #32615 ) ;
#4612=ADVANCED_FACE ( 'NONE', ( #12743 ), #17699, .F. ) ;
#4625=DIRECTION ( 'NONE',  ( 0.000000000000000000, 0.000000000000000000, 1.000000000000000000 ) ) ;
#4626=CARTESIAN_POINT ( 'NONE',  ( 17.00689302767908728, -14.98194955443502252, -14.88746750000000141 ) ) ;
#4650=FACE_OUTER_BOUND ( 'NONE', #24412, .T. ) ;
#4660=CARTESIAN_POINT ( 'NONE',  ( 51.13393739769659874, -56.11618894467899565, 14.21249999999999858 ) ) ;
#4676=CIRCLE ( 'NONE', #8049, 1.000000000000000888 ) ;
#4697=FACE_OUTER_BOUND ( 'NONE', #33299, .T. ) ;
#4720=CARTESIAN_POINT ( 'NONE',  ( 53.63393739769619373, -63.11618894467929408, 11.84999999999999964 ) ) ;
#4721=ADVANCED_FACE ( 'NONE', ( #10885 ), #3309, .F. ) ;
#4741=CARTESIAN_POINT ( 'NONE',  ( 62.63393739769619373, -63.11618894467939356, 11.84999999999999964 ) ) ;
#4790=LINE ( 'NONE', #44620, #29645 ) ;
#4810=ORIENTED_EDGE ( 'NONE', *, *, #31046, .T. ) ;
#4815=ORIENTED_EDGE ( 'NONE', *, *, #49750, .T. ) ;
#4835=EDGE_CURVE ( 'NONE', #6855, #8577, #15062, .T. ) ;
#4868=DIRECTION ( 'NONE',  ( 0.000000000000000000, -1.000000000000000000, 0.000000000000000000 ) ) ;
#4879=ORIENTED_EDGE ( 'NONE', *, *, #19390, .F. ) ;
#4891=EDGE_CURVE ( 'NONE', #18307, #16420, #47055, .T. ) ;
#4943=DIRECTION ( 'NONE',  ( 0.5720614028176835841, -0.4156269377774527984, -0.7071067811865484609 ) ) ;
#4947=AXIS2_PLACEMENT_3D ( 'NONE', #37990, #32999, #37215 ) ;
#4953=EDGE_CURVE ( 'NONE', #51520, #51462, #15055, .T. ) ;
#4966=ADVANCED_FACE ( 'NONE', ( #48070 ), #4290, .T. ) ;
#4971=ORIENTED_EDGE ( 'NONE', *, *, #3081, .F. ) ;
#4992=AXIS2_PLACEMENT_3D ( 'NONE', #28126, #32048, #3536 ) ;
#5002=DIRECTION ( 'NONE',  ( -1.000000000000000000, 0.000000000000000000, 0.000000000000000000 ) ) ;
#5019=LINE ( 'NONE', #13157, #32475 ) ;
#5026=CIRCLE ( 'NONE', #34281, 10.00000000000000711 ) ;
#5034=AXIS2_PLACEMENT_3D ( 'NONE', #39017, #15420, #8068 ) ;
#5051=EDGE_CURVE ( 'NONE', #15767, #18307, #15877, .T. ) ;
#5086=CARTESIAN_POINT ( 'NONE',  ( 26.63393739769619728, -15.61618894467929941, -18.58999999999999986 ) ) ;
#5087=FACE_OUTER_BOUND ( 'NONE', #38255, .T. ) ;
#5106=CARTESIAN_POINT ( 'NONE',  ( 16.13393739769620083, -15.61618894467929941, -5.690000000000000391 ) ) ;
#5123=ORIENTED_EDGE ( 'NONE', *, *, #9783, .T. ) ;
#5137=ADVANCED_FACE ( 'NONE', ( #45106 ), #303, .T. ) ;
#5142=ORIENTED_EDGE ( 'NONE', *, *, #2657, .F. ) ;
#5143=CARTESIAN_POINT ( 'NONE',  ( 51.13393739769620083, 19.38381105532069881, 14.21249999999999858 ) ) ;
#5155=ORIENTED_EDGE ( 'NONE', *, *, #14417, .T. ) ;
#5162=EDGE_CURVE ( 'NONE', #32442, #28421, #40136, .T. ) ;
#5168=CARTESIAN_POINT ( 'NONE',  ( 7.820074255002061214, -21.65656408986289350, -5.690000000000000391 ) ) ;
#5170=FACE_OUTER_BOUND ( 'NONE', #18389, .T. ) ;
#5183=AXIS2_PLACEMENT_3D ( 'NONE', #46554, #10643, #3032 ) ;
#5188=ORIENTED_EDGE ( 'NONE', *, *, #7898, .T. ) ;
#5197=DIRECTION ( 'NONE',  ( 0.000000000000000000, 0.000000000000000000, -1.000000000000000000 ) ) ;
#5199=EDGE_CURVE ( 'NONE', #42670, #47254, #25165, .T. ) ;
#5222=VECTOR ( 'NONE', #34185, 1000.000000000000000 ) ;
#5234=FACE_OUTER_BOUND ( 'NONE', #13150, .T. ) ;
#5239=CARTESIAN_POINT ( 'NONE',  ( -21.36606260230379917, -63.11618894467929408, 11.84999999999999964 ) ) ;
#5291=ORIENTED_EDGE ( 'NONE', *, *, #40410, .T. ) ;
#5322=EDGE_CURVE ( 'NONE', #27172, #14338, #5019, .T. ) ;
#5363=FACE_OUTER_BOUND ( 'NONE', #28462, .T. ) ;
#5385=EDGE_CURVE ( 'NONE', #16578, #40267, #14165, .T. ) ;
#5396=DIRECTION ( 'NONE',  ( 0.000000000000000000, 0.000000000000000000, -1.000000000000000000 ) ) ;
#5441=VERTEX_POINT ( 'NONE', #19642 ) ;
#5443=LINE ( 'NONE', #1755, #26931 ) ;
#5470=DIRECTION ( 'NONE',  ( 0.000000000000000000, 0.000000000000000000, -1.000000000000000000 ) ) ;
#5492=CONICAL_SURFACE ( 'NONE', #19729, 0.6299999999999991163, 0.7853981633974490562 ) ;
#5510=AXIS2_PLACEMENT_3D ( 'NONE', #17511, #41353, #482 ) ;
#5526=DIRECTION ( 'NONE',  ( 0.000000000000000000, 1.000000000000000000, 0.000000000000000000 ) ) ;
#5607=ORIENTED_EDGE ( 'NONE', *, *, #27539, .F. ) ;
#5621=CIRCLE ( 'NONE', #18995, 10.49999999999999822 ) ;
#5623=DIRECTION ( 'NONE',  ( -1.000000000000000000, 0.000000000000000000, 0.000000000000000000 ) ) ;
#5624=CARTESIAN_POINT ( 'NONE',  ( 63.34104417888273986, -63.11618894467939356, 11.14289321881345174 ) ) ;
#5627=EDGE_LOOP ( 'NONE', ( #12895, #24765 ) ) ;
#5635=DIRECTION ( 'NONE',  ( -1.000000000000000000, 0.000000000000000000, 0.000000000000000000 ) ) ;
#5668=ORIENTED_EDGE ( 'NONE', *, *, #16308, .T. ) ;
#5679=VECTOR ( 'NONE', #27099, 1000.000000000000000 ) ;
#5685=EDGE_CURVE ( 'NONE', #29876, #13493, #3241, .T. ) ;
#5717=CARTESIAN_POINT ( 'NONE',  ( 53.63393739769619373, 21.88381105532059934, 17.35000000000000142 ) ) ;
#5724=DIRECTION ( 'NONE',  ( -1.062456999999999985E-16, -7.719205000000000365E-17, -1.000000000000000000 ) ) ;
#5729=FACE_OUTER_BOUND ( 'NONE', #31231, .T. ) ;
#5752=LINE ( 'NONE', #25897, #23854 ) ;
#5760=CARTESIAN_POINT ( 'NONE',  ( 53.63393739769619373, -53.11618894467930119, 10.84999999999999964 ) ) ;
#5781=ADVANCED_FACE ( 'NONE', ( #32181 ), #32434, .T. ) ;
#5826=ORIENTED_EDGE ( 'NONE', *, *, #51702, .F. ) ;
#5857=DIRECTION ( 'NONE',  ( -1.000000000000000000, 0.000000000000000000, 0.000000000000000000 ) ) ;
#5864=FACE_OUTER_BOUND ( 'NONE', #36642, .T. ) ;
#5874=EDGE_LOOP ( 'NONE', ( #13827, #14612, #32067, #43067, #43760, #44425 ) ) ;
#5880=AXIS2_PLACEMENT_3D ( 'NONE', #47330, #11421, #27386 ) ;
#5897=DIRECTION ( 'NONE',  ( -0.8090169943749453418, 0.5877852522924759127, 0.000000000000000000 ) ) ;
#5900=CARTESIAN_POINT ( 'NONE',  ( 37.86285195093699940, -15.61618894467929763, 9.349999999999999645 ) ) ;
#5934=ORIENTED_EDGE ( 'NONE', *, *, #10066, .T. ) ;
#5943=CARTESIAN_POINT ( 'NONE',  ( -21.36606260230379917, -63.11618894467929408, 16.35000000000000142 ) ) ;
#5944=CARTESIAN_POINT ( 'NONE',  ( -31.07316938349034885, -53.11618894467930119, 11.14289321881345352 ) ) ;
#5968=DIRECTION ( 'NONE',  ( 0.000000000000000000, 0.000000000000000000, -1.000000000000000000 ) ) ;
#5974=DIRECTION ( 'NONE',  ( 0.000000000000000000, 0.000000000000000000, 1.000000000000000000 ) ) ;
#6006=ORIENTED_EDGE ( 'NONE', *, *, #51280, .T. ) ;
#6028=EDGE_CURVE ( 'NONE', #49041, #49436, #33307, .T. ) ;
#6040=EDGE_CURVE ( 'NONE', #46863, #12957, #2448, .T. ) ;
#6044=VERTEX_POINT ( 'NONE', #563 ) ;
#6055=ORIENTED_EDGE ( 'NONE', *, *, #14626, .T. ) ;
#6066=LINE ( 'NONE', #42751, #35952 ) ;
#6068=DIRECTION ( 'NONE',  ( 0.000000000000000000, 0.000000000000000000, -1.000000000000000000 ) ) ;
#6082=EDGE_CURVE ( 'NONE', #16397, #24197, #50968, .T. ) ;
#6093=CARTESIAN_POINT ( 'NONE',  ( -21.36606260230379917, -53.11618894467930119, 16.35000000000000142 ) ) ;
#6101=DIRECTION ( 'NONE',  ( 1.000000000000000000, 0.000000000000000000, 0.000000000000000000 ) ) ;
#6110=CIRCLE ( 'NONE', #219, 13.50000000000000178 ) ;
#6116=CIRCLE ( 'NONE', #31183, 35.00000000000000000 ) ;
#6130=FACE_OUTER_BOUND ( 'NONE', #42871, .T. ) ;
#6145=DIRECTION ( 'NONE',  ( -0.5877852522924764678, 0.8090169943749450088, 0.000000000000000000 ) ) ;
#6170=ORIENTED_EDGE ( 'NONE', *, *, #8917, .F. ) ;
#6179=DIRECTION ( 'NONE',  ( -1.000000000000000000, 0.000000000000000000, 0.000000000000000000 ) ) ;
#6186=CIRCLE ( 'NONE', #27893, 1.000000000000000888 ) ;
#6215=DIRECTION ( 'NONE',  ( 0.7071067811865473507, 0.7071067811865476838, 0.000000000000000000 ) ) ;
#6228=CARTESIAN_POINT ( 'NONE',  ( 51.13393739769659874, -50.61618894467899565, 16.85000000000000142 ) ) ;
#6234=DIRECTION ( 'NONE',  ( -0.8090169943749466741, -0.5877852522924741363, 0.000000000000000000 ) ) ;
#6238=CARTESIAN_POINT ( 'NONE',  ( 53.63393739769619373, 30.88381105532059934, 16.35000000000000142 ) ) ;
#6270=EDGE_CURVE ( 'NONE', #6972, #6855, #29207, .T. ) ;
#6301=DIRECTION ( 'NONE',  ( 1.000000000000000000, 0.000000000000000000, 0.000000000000000000 ) ) ;
#6352=LINE ( 'NONE', #41727, #47382 ) ;
#6375=VERTEX_POINT ( 'NONE', #30142 ) ;
#6389=DIRECTION ( 'NONE',  ( 0.000000000000000000, -1.000000000000000000, 0.000000000000000000 ) ) ;
#6406=AXIS2_PLACEMENT_3D ( 'NONE', #34091, #46189, #6868 ) ;
#6418=AXIS2_PLACEMENT_3D ( 'NONE', #36891, #11773, #47924 ) ;
#6424=AXIS2_PLACEMENT_3D ( 'NONE', #33415, #21611, #46016 ) ;
#6443=VERTEX_POINT ( 'NONE', #33565 ) ;
#6488=DIRECTION ( 'NONE',  ( 1.000000000000000000, 0.000000000000000000, 0.000000000000000000 ) ) ;
#6489=DIRECTION ( 'NONE',  ( 1.000000000000000000, 0.000000000000000000, 0.000000000000000000 ) ) ;
#6533=DIRECTION ( 'NONE',  ( 0.000000000000000000, 0.000000000000000000, 1.000000000000000000 ) ) ;
#6569=ORIENTED_EDGE ( 'NONE', *, *, #50685, .F. ) ;
#6585=CARTESIAN_POINT ( 'NONE',  ( 16.13393739769620083, -15.61618894467929941, -18.58999999999999986 ) ) ;
#6596=DIRECTION ( 'NONE',  ( 0.000000000000000000, 0.000000000000000000, 1.000000000000000000 ) ) ;
#6643=DIRECTION ( 'NONE',  ( -0.7071067811865475727, 0.000000000000000000, 0.7071067811865475727 ) ) ;
#6664=EDGE_LOOP ( 'NONE', ( #3512, #33094, #35932, #24447, #30271, #49934 ) ) ;
#6665=CARTESIAN_POINT ( 'NONE',  ( -31.07316938349034885, -53.11618894467940066, 17.05710678118654755 ) ) ;
#6683=VECTOR ( 'NONE', #4868, 1000.000000000000000 ) ;
#6688=EDGE_CURVE ( 'NONE', #26597, #44905, #19972, .T. ) ;
#6696=CARTESIAN_POINT ( 'NONE',  ( 29.63393739769620083, -15.61618894467929941, 4.349999999999999645 ) ) ;
#6710=CIRCLE ( 'NONE', #43518, 21.72891455324079857 ) ;
#6719=CIRCLE ( 'NONE', #11735, 6.100000000000001421 ) ;
#6727=CARTESIAN_POINT ( 'NONE',  ( 16.13393739769620083, -15.61618894467929941, -9.721247897589949005 ) ) ;
#6732=CARTESIAN_POINT ( 'NONE',  ( 51.64361810415240939, 19.75411576426495586, 11.97999999999999865 ) ) ;
#6734=EDGE_CURVE ( 'NONE', #47505, #18529, #12768, .T. ) ;
#6745=ORIENTED_EDGE ( 'NONE', *, *, #35259, .F. ) ;
#6755=AXIS2_PLACEMENT_3D ( 'NONE', #25183, #30152, #50353 ) ;
#6772=DIRECTION ( 'NONE',  ( 0.000000000000000000, 0.000000000000000000, 1.000000000000000000 ) ) ;
#6820=EDGE_CURVE ( 'NONE', #6962, #26597, #40973, .T. ) ;
#6855=VERTEX_POINT ( 'NONE', #41532 ) ;
#6868=DIRECTION ( 'NONE',  ( 0.000000000000000000, 1.000000000000000000, 0.000000000000000000 ) ) ;
#6898=VERTEX_POINT ( 'NONE', #37595 ) ;
#6904=DIRECTION ( 'NONE',  ( 0.000000000000000000, 0.000000000000000000, 1.000000000000000000 ) ) ;
#6905=CIRCLE ( 'NONE', #4373, 9.000000000000007105 ) ;
#6909=VECTOR ( 'NONE', #13015, 1000.000000000000000 ) ;
#6910=FACE_BOUND ( 'NONE', #43764, .T. ) ;
#6915=DIRECTION ( 'NONE',  ( -1.000000000000000000, 0.000000000000000000, 0.000000000000000000 ) ) ;
#6941=LINE ( 'NONE', #29274, #15616 ) ;
#6962=VERTEX_POINT ( 'NONE', #15574 ) ;
#6965=ADVANCED_FACE ( 'NONE', ( #22641 ), #34953, .T. ) ;
#6972=VERTEX_POINT ( 'NONE', #38658 ) ;
#6977=DIRECTION ( 'NONE',  ( -1.000000000000000000, 0.000000000000000000, 0.000000000000000000 ) ) ;
#7003=ORIENTED_EDGE ( 'NONE', *, *, #18309, .T. ) ;
#7017=ORIENTED_EDGE ( 'NONE', *, *, #47470, .T. ) ;
#7034=EDGE_CURVE ( 'NONE', #18843, #24877, #35915, .T. ) ;
#7044=DIRECTION ( 'NONE',  ( 0.000000000000000000, 0.000000000000000000, -1.000000000000000000 ) ) ;
#7058=CARTESIAN_POINT ( 'NONE',  ( 35.63393739769620083, -15.61618894467929941, -14.68999999999999950 ) ) ;
#7062=AXIS2_PLACEMENT_3D ( 'NONE', #6585, #23061, #30412 ) ;
#7071=ORIENTED_EDGE ( 'NONE', *, *, #19648, .T. ) ;
#7084=AXIS2_PLACEMENT_3D ( 'NONE', #4741, #8424, #16801 ) ;
#7104=ORIENTED_EDGE ( 'NONE', *, *, #47577, .F. ) ;
#7113=EDGE_LOOP ( 'NONE', ( #10495, #7242, #44003, #22338, #10690, #19663, #10706 ) ) ;
#7120=VECTOR ( 'NONE', #14725, 1000.000000000000000 ) ;
#7130=DIRECTION ( 'NONE',  ( -0.5720614028176840282, -0.4156269377774530760, 0.7071067811865479058 ) ) ;
#7132=ORIENTED_EDGE ( 'NONE', *, *, #26058, .F. ) ;
#7135=CARTESIAN_POINT ( 'NONE',  ( 51.13393739769659874, -50.61618894467899565, 17.35000000000000142 ) ) ;
#7152=DIRECTION ( 'NONE',  ( -1.000000000000000000, -2.362305513541788125E-32, -1.430038757655089944E-15 ) ) ;
#7155=ORIENTED_EDGE ( 'NONE', *, *, #16488, .T. ) ;
#7175=CIRCLE ( 'NONE', #44014, 10.00000000000000711 ) ;
#7190=TOROIDAL_SURFACE ( 'NONE', #5510, 17.19098300429530113, 0.5000000000822009127 ) ;
#7203=EDGE_LOOP ( 'NONE', ( #7626, #45723, #48387, #45109, #1397 ) ) ;
#7229=ORIENTED_EDGE ( 'NONE', *, *, #39535, .F. ) ;
#7242=ORIENTED_EDGE ( 'NONE', *, *, #41390, .T. ) ;
#7251=CYLINDRICAL_SURFACE ( 'NONE', #37219, 11.00000000000000000 ) ;
#7257=ORIENTED_EDGE ( 'NONE', *, *, #14417, .F. ) ;
#7259=ORIENTED_EDGE ( 'NONE', *, *, #20618, .F. ) ;
#7289=ORIENTED_EDGE ( 'NONE', *, *, #50569, .T. ) ;
#7317=LINE ( 'NONE', #39283, #11406 ) ;
#7321=ADVANCED_FACE ( 'NONE', ( #29154 ), #41792, .F. ) ;
#7326=CARTESIAN_POINT ( 'NONE',  ( -14.01196063605392439, -54.14290045843446109, 10.84999999999999964 ) ) ;
#7339=EDGE_CURVE ( 'NONE', #41355, #33328, #1624, .T. ) ;
#7343=VERTEX_POINT ( 'NONE', #33076 ) ;
#7344=EDGE_CURVE ( 'NONE', #26468, #49915, #30891, .T. ) ;
#7351=DIRECTION ( 'NONE',  ( 1.000000000000000000, 0.000000000000000000, 0.000000000000000000 ) ) ;
#7371=DIRECTION ( 'NONE',  ( 0.000000000000000000, 0.000000000000000000, -1.000000000000000000 ) ) ;
#7403=DIRECTION ( 'NONE',  ( 0.000000000000000000, 0.000000000000000000, 1.000000000000000000 ) ) ;
#7461=ORIENTED_EDGE ( 'NONE', *, *, #3081, .T. ) ;
#7475=ORIENTED_EDGE ( 'NONE', *, *, #49913, .T. ) ;
#7481=ORIENTED_EDGE ( 'NONE', *, *, #46636, .F. ) ;
#7496=AXIS2_PLACEMENT_3D ( 'NONE', #24518, #13037, #693 ) ;
#7513=CARTESIAN_POINT ( 'NONE',  ( 51.13393739769620083, 19.38381105532069881, 16.85000000000000142 ) ) ;
#7519=VERTEX_POINT ( 'NONE', #21164 ) ;
#7534=CIRCLE ( 'NONE', #27599, 4.649999999999999467 ) ;
#7572=CIRCLE ( 'NONE', #51075, 5.499999999999998224 ) ;
#7573=AXIS2_PLACEMENT_3D ( 'NONE', #39642, #35709, #8187 ) ;
#7579=DIRECTION ( 'NONE',  ( 1.000000000000000000, 0.000000000000000000, 0.000000000000000000 ) ) ;
#7588=CARTESIAN_POINT ( 'NONE',  ( 53.63393739769619373, 31.88381105532059934, 11.84999999999999964 ) ) ;
#7626=ORIENTED_EDGE ( 'NONE', *, *, #49750, .F. ) ;
#7645=FACE_OUTER_BOUND ( 'NONE', #725, .T. ) ;
#7651=FACE_OUTER_BOUND ( 'NONE', #3588, .T. ) ;
#7669=DIRECTION ( 'NONE',  ( -0.000000000000000000, -1.000000000000000000, -0.000000000000000000 ) ) ;
#7677=DIRECTION ( 'NONE',  ( 0.000000000000000000, 0.000000000000000000, -1.000000000000000000 ) ) ;
#7690=CIRCLE ( 'NONE', #36957, 9.000000000000007105 ) ;
#7702=EDGE_CURVE ( 'NONE', #18529, #50796, #34592, .T. ) ;
#7704=CARTESIAN_POINT ( 'NONE',  ( 16.13393739769620083, -15.61618894467929941, 9.349999999999999645 ) ) ;
#7710=ORIENTED_EDGE ( 'NONE', *, *, #14710, .T. ) ;
#7723=CIRCLE ( 'NONE', #15279, 20.00000000000000000 ) ;
#7743=EDGE_LOOP ( 'NONE', ( #48118, #24371, #21226, #33620, #45693, #35147 ) ) ;
#7763=ADVANCED_FACE ( 'NONE', ( #30574 ), #40470, .F. ) ;
#7785=EDGE_LOOP ( 'NONE', ( #5142, #17185, #4346, #38645, #13985 ) ) ;
#7788=ORIENTED_EDGE ( 'NONE', *, *, #47296, .T. ) ;
#7808=DIRECTION ( 'NONE',  ( 1.000000000000000000, 0.000000000000000000, 0.000000000000000000 ) ) ;
#7819=ORIENTED_EDGE ( 'NONE', *, *, #14254, .T. ) ;
#7821=AXIS2_PLACEMENT_3D ( 'NONE', #16088, #44906, #878 ) ;
#7867=AXIS2_PLACEMENT_3D ( 'NONE', #32545, #15825, #4285 ) ;
#7869=EDGE_CURVE ( 'NONE', #49041, #42488, #37223, .T. ) ;
#7871=DIRECTION ( 'NONE',  ( 0.000000000000000000, 9.718338800990680596E-16, -1.000000000000000000 ) ) ;
#7881=DIRECTION ( 'NONE',  ( 0.000000000000000000, 0.000000000000000000, 1.000000000000000000 ) ) ;
#7892=AXIS2_PLACEMENT_3D ( 'NONE', #51467, #11382, #46256 ) ;
#7898=EDGE_CURVE ( 'NONE', #31235, #42670, #9512, .T. ) ;
#7910=DIRECTION ( 'NONE',  ( -1.000000000000000000, 0.000000000000000000, 0.000000000000000000 ) ) ;
#7918=DIRECTION ( 'NONE',  ( 0.000000000000000000, 0.000000000000000000, -1.000000000000000000 ) ) ;
#7929=ORIENTED_EDGE ( 'NONE', *, *, #35357, .F. ) ;
#7936=STYLED_ITEM ( 'NONE', ( #42372 ), #9246 ) ;
#8005=FACE_OUTER_BOUND ( 'NONE', #21110, .T. ) ;
#8043=CIRCLE ( 'NONE', #10566, 11.00000000000000000 ) ;
#8047=DIRECTION ( 'NONE',  ( 0.000000000000000000, 0.000000000000000000, -1.000000000000000000 ) ) ;
#8049=AXIS2_PLACEMENT_3D ( 'NONE', #47733, #35146, #39607 ) ;
#8067=DIRECTION ( 'NONE',  ( 1.224646799147353207E-16, 1.000000000000000000, -0.000000000000000000 ) ) ;
#8068=DIRECTION ( 'NONE',  ( -1.000000000000000000, 0.000000000000000000, 0.000000000000000000 ) ) ;
#8074=ORIENTED_EDGE ( 'NONE', *, *, #26592, .T. ) ;
#8092=ORIENTED_EDGE ( 'NONE', *, *, #37210, .F. ) ;
#8097=DIRECTION ( 'NONE',  ( -1.000000000000000000, 0.000000000000000000, 0.000000000000000000 ) ) ;
#8110=CARTESIAN_POINT ( 'NONE',  ( 34.13393739769620083, -15.61618894467929941, -20.58999999999999986 ) ) ;
#8124=ORIENTED_EDGE ( 'NONE', *, *, #25888, .F. ) ;
#8135=AXIS2_PLACEMENT_3D ( 'NONE', #42653, #47112, #30571 ) ;
#8139=FACE_OUTER_BOUND ( 'NONE', #32501, .T. ) ;
#8142=FACE_OUTER_BOUND ( 'NONE', #16654, .T. ) ;
#8148=EDGE_CURVE ( 'NONE', #19682, #19506, #39698, .T. ) ;
#8165=EDGE_LOOP ( 'NONE', ( #2581, #21411, #43327, #36202 ) ) ;
#8180=CIRCLE ( 'NONE', #39157, 1.000000000000000888 ) ;
#8186=ORIENTED_EDGE ( 'NONE', *, *, #42182, .F. ) ;
#8187=DIRECTION ( 'NONE',  ( 0.000000000000000000, -1.000000000000000000, 0.000000000000000000 ) ) ;
#8191=CARTESIAN_POINT ( 'NONE',  ( 16.13393739769620083, -15.61618894467929941, -18.35000000000000142 ) ) ;
#8197=ADVANCED_FACE ( 'NONE', ( #21233, #46154 ), #10241, .T. ) ;
#8244=DIRECTION ( 'NONE',  ( 1.000000000000000000, 0.000000000000000000, 0.000000000000000000 ) ) ;
#8306=DIRECTION ( 'NONE',  ( 0.000000000000000000, 0.000000000000000000, -1.000000000000000000 ) ) ;
#8308=CARTESIAN_POINT ( 'NONE',  ( 51.13393739769620083, 19.38381105532069881, 10.84999999999999964 ) ) ;
#8321=EDGE_CURVE ( 'NONE', #15443, #371, #49760, .T. ) ;
#8343=ORIENTED_EDGE ( 'NONE', *, *, #4835, .T. ) ;
#8360=VECTOR ( 'NONE', #18728, 1000.000000000000000 ) ;
#8390=AXIS2_PLACEMENT_3D ( 'NONE', #4127, #449, #24795 ) ;
#8399=DIRECTION ( 'NONE',  ( 0.000000000000000000, 0.000000000000000000, 1.000000000000000000 ) ) ;
#8424=DIRECTION ( 'NONE',  ( 0.000000000000000000, 1.000000000000000000, 0.000000000000000000 ) ) ;
#8451=ADVANCED_FACE ( 'NONE', ( #25265 ), #41366, .T. ) ;
#8454=ORIENTED_EDGE ( 'NONE', *, *, #9783, .F. ) ;
#8462=CARTESIAN_POINT ( 'NONE',  ( -18.86606260230390220, 19.38381105532060289, 17.35000000000000142 ) ) ;
#8469=CARTESIAN_POINT ( 'NONE',  ( -21.36606260230379917, 21.88381105532059934, 17.35000000000000142 ) ) ;
#8485=CARTESIAN_POINT ( 'NONE',  ( -21.36606260230379917, -62.82329572586585442, 17.05710678118654400 ) ) ;
#8503=ORIENTED_EDGE ( 'NONE', *, *, #51861, .T. ) ;
#8504=CIRCLE ( 'NONE', #50370, 0.5000000000000004441 ) ;
#8506=CIRCLE ( 'NONE', #37796, 5.999999999999998224 ) ;
#8509=CARTESIAN_POINT ( 'NONE',  ( -28.43713041416927467, 28.95487886718607129, 11.84999999999999964 ) ) ;
#8513=EDGE_CURVE ( 'NONE', #33500, #15767, #45566, .T. ) ;
#8515=EDGE_CURVE ( 'NONE', #12957, #13595, #28788, .T. ) ;
#8557=DIRECTION ( 'NONE',  ( -0.7071067811865476838, -0.7071067811865473507, 0.000000000000000000 ) ) ;
#8558=VERTEX_POINT ( 'NONE', #4271 ) ;
#8575=ADVANCED_FACE ( 'NONE', ( #20241 ), #35506, .T. ) ;
#8577=VERTEX_POINT ( 'NONE', #340 ) ;
#8585=CARTESIAN_POINT ( 'NONE',  ( -21.36606260230379917, 31.88381105532059934, 11.84999999999999964 ) ) ;
#8592=ORIENTED_EDGE ( 'NONE', *, *, #29623, .F. ) ;
#8610=DIRECTION ( 'NONE',  ( 0.000000000000000000, 0.000000000000000000, -1.000000000000000000 ) ) ;
#8618=EDGE_CURVE ( 'NONE', #4597, #13604, #4790, .T. ) ;
#8620=VERTEX_POINT ( 'NONE', #20758 ) ;
#8628=FACE_OUTER_BOUND ( 'NONE', #39131, .T. ) ;
#8647=DIRECTION ( 'NONE',  ( -1.000000000000000000, 0.000000000000000000, 0.000000000000000000 ) ) ;
#8687=CARTESIAN_POINT ( 'NONE',  ( 62.63393739769619373, -39.36618894467940066, 16.35000000000000142 ) ) ;
#8728=FACE_OUTER_BOUND ( 'NONE', #22182, .T. ) ;
#8773=CARTESIAN_POINT ( 'NONE',  ( 55.98803936394586600, 15.85709954156585333, 10.84999999999999964 ) ) ;
#8788=CARTESIAN_POINT ( 'NONE',  ( -28.43713041416927823, -60.18725675654476959, 16.35000000000000142 ) ) ;
#8804=VERTEX_POINT ( 'NONE', #33596 ) ;
#8812=CARTESIAN_POINT ( 'NONE',  ( -30.36606260230379917, 21.88381105532059934, 11.84999999999999964 ) ) ;
#8816=CIRCLE ( 'NONE', #48162, 17.19098300562509962 ) ;
#8819=ORIENTED_EDGE ( 'NONE', *, *, #13620, .T. ) ;
#8834=ORIENTED_EDGE ( 'NONE', *, *, #22027, .T. ) ;
#8892=DIRECTION ( 'NONE',  ( 1.000000000000000000, 0.000000000000000000, 0.000000000000000000 ) ) ;
#8898=VERTEX_POINT ( 'NONE', #26761 ) ;
#8917=EDGE_CURVE ( 'NONE', #18483, #2702, #11060, .T. ) ;
#8942=EDGE_CURVE ( 'NONE', #28918, #44905, #34100, .T. ) ;
#8946=EDGE_LOOP ( 'NONE', ( #8074, #19882, #31167, #41628, #26130, #26923, #11996 ) ) ;
#8950=DIRECTION ( 'NONE',  ( -1.000000000000000000, 0.000000000000000000, 0.000000000000000000 ) ) ;
#8970=AXIS2_PLACEMENT_3D ( 'NONE', #34764, #27162, #11201 ) ;
#9011=ORIENTED_EDGE ( 'NONE', *, *, #36468, .T. ) ;
#9032=VERTEX_POINT ( 'NONE', #47099 ) ;
#9043=DIRECTION ( 'NONE',  ( -1.000000000000000000, 0.000000000000000000, 0.000000000000000000 ) ) ;
#9053=EDGE_CURVE ( 'NONE', #235, #1350, #1234, .T. ) ;
#9058=ADVANCED_FACE ( 'NONE', ( #35277 ), #7251, .F. ) ;
#9103=CARTESIAN_POINT ( 'NONE',  ( 16.13393739769620083, -15.61618894467929941, -14.68999999999999950 ) ) ;
#9105=ADVANCED_FACE ( 'NONE', ( #10669 ), #39723, .T. ) ;
#9136=ORIENTED_EDGE ( 'NONE', *, *, #14940, .F. ) ;
#9157=ORIENTED_EDGE ( 'NONE', *, *, #6040, .F. ) ;
#9176=AXIS2_PLACEMENT_3D ( 'NONE', #32092, #24223, #16134 ) ;
#9178=AXIS2_PLACEMENT_3D ( 'NONE', #1544, #1801, #50020 ) ;
#9192=ORIENTED_EDGE ( 'NONE', *, *, #29710, .F. ) ;
#9239=ORIENTED_EDGE ( 'NONE', *, *, #188, .T. ) ;
#9246=MANIFOLD_SOLID_BREP ( 'Stock-MAS-691-1', #36027 ) ;
#9254=DIRECTION ( 'NONE',  ( 0.000000000000000000, 0.000000000000000000, 1.000000000000000000 ) ) ;
#9256=CARTESIAN_POINT ( 'NONE',  ( 15.26098176771331261, -14.98194955443502252, -9.392532499999980189 ) ) ;
#9273=DIRECTION ( 'NONE',  ( 0.000000000000000000, 0.000000000000000000, 1.000000000000000000 ) ) ;
#9346=ADVANCED_FACE ( 'NONE', ( #8005 ), #11693, .T. ) ;
#9355=ORIENTED_EDGE ( 'NONE', *, *, #6028, .T. ) ;
#9356=FACE_OUTER_BOUND ( 'NONE', #6664, .T. ) ;
#9392=ORIENTED_EDGE ( 'NONE', *, *, #16449, .T. ) ;
#9420=CARTESIAN_POINT ( 'NONE',  ( -18.86606260230390220, 19.38381105532060289, 16.85000000000000142 ) ) ;
#9454=ORIENTED_EDGE ( 'NONE', *, *, #29710, .T. ) ;
#9491=DIRECTION ( 'NONE',  ( -1.000000000000000000, -2.362305513541788125E-32, -1.430038757655089944E-15 ) ) ;
#9504=CARTESIAN_POINT ( 'NONE',  ( 16.13393739769620083, -15.61618894467929941, 10.84999999999999964 ) ) ;
#9510=CARTESIAN_POINT ( 'NONE',  ( -2.727866001178802513, -15.61618894467929941, 17.07360679774999923 ) ) ;
#9512=CIRCLE ( 'NONE', #37112, 4.999999999969890752 ) ;
#9518=CIRCLE ( 'NONE', #12850, 9.999999999999998224 ) ;
#9542=EDGE_LOOP ( 'NONE', ( #35628, #18676, #50838, #32161 ) ) ;
#9549=ORIENTED_EDGE ( 'NONE', *, *, #35058, .F. ) ;
#9556=DIRECTION ( 'NONE',  ( 1.000000000000000000, 0.000000000000000000, 0.000000000000000000 ) ) ;
#9595=VERTEX_POINT ( 'NONE', #6665 ) ;
#9609=DIRECTION ( 'NONE',  ( 0.000000000000000000, -1.000000000000000000, 0.000000000000000000 ) ) ;
#9625=EDGE_CURVE ( 'NONE', #11039, #13741, #50172, .T. ) ;
#9626=DIRECTION ( 'NONE',  ( -1.000000000000000000, 0.000000000000000000, 0.000000000000000000 ) ) ;
#9628=CARTESIAN_POINT ( 'NONE',  ( 16.13393739769620083, -15.61618894467929941, -16.68902128623620129 ) ) ;
#9634=CARTESIAN_POINT ( 'NONE',  ( 16.13393739769620083, -15.61618894467929941, 9.349999999999999645 ) ) ;
#9650=DIRECTION ( 'NONE',  ( 0.000000000000000000, 0.000000000000000000, -1.000000000000000000 ) ) ;
#9743=ORIENTED_EDGE ( 'NONE', *, *, #47389, .T. ) ;
#9748=VECTOR ( 'NONE', #6101, 1000.000000000000000 ) ;
#9775=LINE ( 'NONE', #42003, #19795 ) ;
#9779=DIRECTION ( 'NONE',  ( -0.7071067811865475727, 0.000000000000000000, -0.7071067811865475727 ) ) ;
#9780=FACE_OUTER_BOUND ( 'NONE', #7743, .T. ) ;
#9783=EDGE_CURVE ( 'NONE', #6972, #31235, #25521, .T. ) ;
#9787=DIRECTION ( 'NONE',  ( 0.000000000000000000, 0.000000000000000000, -1.000000000000000000 ) ) ;
#9793=AXIS2_PLACEMENT_3D ( 'NONE', #9504, #45400, #41453 ) ;
#9794=EDGE_LOOP ( 'NONE', ( #7229, #15648 ) ) ;
#9804=EDGE_CURVE ( 'NONE', #1782, #21433, #3769, .T. ) ;
#9813=CARTESIAN_POINT ( 'NONE',  ( 16.13393739769620083, -15.61618894467929941, -6.189999999999999503 ) ) ;
#9841=CARTESIAN_POINT ( 'NONE',  ( 51.13393739769620083, 19.38381105532069881, 11.97999999999999865 ) ) ;
#9849=ORIENTED_EDGE ( 'NONE', *, *, #29038, .F. ) ;
#9862=ORIENTED_EDGE ( 'NONE', *, *, #39208, .T. ) ;
#9920=DIRECTION ( 'NONE',  ( 0.000000000000000000, 0.000000000000000000, -1.000000000000000000 ) ) ;
#9922=ORIENTED_EDGE ( 'NONE', *, *, #35627, .T. ) ;
#9924=AXIS2_PLACEMENT_3D ( 'NONE', #32843, #36275, #48089 ) ;
#9959=FACE_OUTER_BOUND ( 'NONE', #40989, .T. ) ;
#9967=FACE_OUTER_BOUND ( 'NONE', #31922, .T. ) ;
#9988=VERTEX_POINT ( 'NONE', #36041 ) ;
#9996=ORIENTED_EDGE ( 'NONE', *, *, #6082, .F. ) ;
#10003=AXIS2_PLACEMENT_3D ( 'NONE', #1128, #17123, #21286 ) ;
#10027=DIRECTION ( 'NONE',  ( 0.000000000000000000, 0.000000000000000000, -1.000000000000000000 ) ) ;
#10028=DIRECTION ( 'NONE',  ( -1.000000000000000000, 0.000000000000000000, 0.000000000000000000 ) ) ;
#10041=DIRECTION ( 'NONE',  ( 0.000000000000000000, 0.000000000000000000, 1.000000000000000000 ) ) ;
#10048=EDGE_CURVE ( 'NONE', #6044, #42020, #26423, .T. ) ;
#10066=EDGE_CURVE ( 'NONE', #3068, #30599, #33116, .T. ) ;
#10072=CARTESIAN_POINT ( 'NONE',  ( 16.13393739769620083, -15.61618894467929941, -8.849999999999999645 ) ) ;
#10073=CIRCLE ( 'NONE', #2546, 10.27649999999999686 ) ;
#10081=CARTESIAN_POINT ( 'NONE',  ( -21.36606260230379917, -62.11618894467930119, 10.84999999999999964 ) ) ;
#10090=FACE_OUTER_BOUND ( 'NONE', #50471, .T. ) ;
#10095=CARTESIAN_POINT ( 'NONE',  ( -21.36606260230379917, -53.11618894467930119, 17.35000000000000142 ) ) ;
#10104=DIRECTION ( 'NONE',  ( 0.000000000000000000, 0.000000000000000000, 1.000000000000000000 ) ) ;
#10107=DIRECTION ( 'NONE',  ( 1.000000000000000000, 0.000000000000000000, 0.000000000000000000 ) ) ;
#10165=CARTESIAN_POINT ( 'NONE',  ( 0.8744179034472430168, -26.70287881417802467, 17.07360679774999923 ) ) ;
#10168=ORIENTED_EDGE ( 'NONE', *, *, #42022, .F. ) ;
#10188=CONICAL_SURFACE ( 'NONE', #19820, 0.6299999999999977840, 0.7853981633974476129 ) ;
#10209=DIRECTION ( 'NONE',  ( 0.4156269377774581275, -0.5720614028176801424, 0.7071067811865482389 ) ) ;
#10215=CARTESIAN_POINT ( 'NONE',  ( -31.36606260230380272, 21.88381105532059934, 11.84999999999999964 ) ) ;
#10241=PLANE ( 'NONE',  #48076 ) ;
#10270=CARTESIAN_POINT ( 'NONE',  ( 24.44780054039034667, -21.65656408986289705, -18.58999999999999986 ) ) ;
#10285=ORIENTED_EDGE ( 'NONE', *, *, #46075, .F. ) ;
#10294=DIRECTION ( 'NONE',  ( 0.000000000000000000, 0.000000000000000000, 1.000000000000000000 ) ) ;
#10298=AXIS2_PLACEMENT_3D ( 'NONE', #17054, #33008, #49031 ) ;
#10300=DIRECTION ( 'NONE',  ( 0.000000000000000000, 0.000000000000000000, 1.000000000000000000 ) ) ;
#10309=DIRECTION ( 'NONE',  ( 0.000000000000000000, -1.000000000000000000, 0.000000000000000000 ) ) ;
#10341=VERTEX_POINT ( 'NONE', #14529 ) ;
#10346=DIRECTION ( 'NONE',  ( 0.000000000000000000, 1.000000000000000000, 0.000000000000000000 ) ) ;
#10347=DIRECTION ( 'NONE',  ( 7.719205000000000365E-17, 1.062456999999999985E-16, 1.000000000000000000 ) ) ;
#10348=DIRECTION ( 'NONE',  ( 0.000000000000000000, 6.470469973722704271E-12, 1.000000000000000000 ) ) ;
#10355=AXIS2_PLACEMENT_3D ( 'NONE', #47935, #35617, #16208 ) ;
#10408=EDGE_CURVE ( 'NONE', #17150, #47191, #46582, .T. ) ;
#10419=DIRECTION ( 'NONE',  ( 0.000000000000000000, 0.000000000000000000, 1.000000000000000000 ) ) ;
#10429=ORIENTED_EDGE ( 'NONE', *, *, #51512, .T. ) ;
#10495=ORIENTED_EDGE ( 'NONE', *, *, #8515, .T. ) ;
#10501=CARTESIAN_POINT ( 'NONE',  ( 6.365687397696198957, -15.61618894467929941, -18.08174999999999955 ) ) ;
#10511=ORIENTED_EDGE ( 'NONE', *, *, #36196, .T. ) ;
#10526=EDGE_LOOP ( 'NONE', ( #3326, #33878, #43112, #7132 ) ) ;
#10566=AXIS2_PLACEMENT_3D ( 'NONE', #42510, #6596, #18306 ) ;
#10622=ORIENTED_EDGE ( 'NONE', *, *, #50099, .T. ) ;
#10640=CIRCLE ( 'NONE', #46633, 6.100000000000001421 ) ;
#10643=DIRECTION ( 'NONE',  ( 0.000000000000000000, 0.000000000000000000, 1.000000000000000000 ) ) ;
#10654=CARTESIAN_POINT ( 'NONE',  ( -21.36606260230379917, -53.11618894467930119, 11.84999999999999964 ) ) ;
#10656=CARTESIAN_POINT ( 'NONE',  ( -18.86606260230360022, -50.61618894467959962, 16.85000000000000142 ) ) ;
#10660=ORIENTED_EDGE ( 'NONE', *, *, #18802, .F. ) ;
#10669=FACE_OUTER_BOUND ( 'NONE', #7113, .T. ) ;
#10679=DIRECTION ( 'NONE',  ( 1.000000000000000000, 0.000000000000000000, 0.000000000000000000 ) ) ;
#10689=CYLINDRICAL_SURFACE ( 'NONE', #43989, 5.499999999999998224 ) ;
#10690=ORIENTED_EDGE ( 'NONE', *, *, #16449, .F. ) ;
#10702=DIRECTION ( 'NONE',  ( 0.000000000000000000, 1.000000000000000000, 0.000000000000000000 ) ) ;
#10706=ORIENTED_EDGE ( 'NONE', *, *, #6040, .T. ) ;
#10723=AXIS2_PLACEMENT_3D ( 'NONE', #32045, #48067, #28124 ) ;
#10729=DIRECTION ( 'NONE',  ( 0.000000000000000000, -1.000000000000000000, 0.000000000000000000 ) ) ;
#10741=CARTESIAN_POINT ( 'NONE',  ( -21.36606260230379917, -63.11618894467929408, 11.84999999999999964 ) ) ;
#10768=CARTESIAN_POINT ( 'NONE',  ( -15.33935108854906026, 14.52970908907092529, 17.35000000000000142 ) ) ;
#10776=CARTESIAN_POINT ( 'NONE',  ( -21.36606260230379917, 21.88381105532059934, 10.84999999999999964 ) ) ;
#10784=ORIENTED_EDGE ( 'NONE', *, *, #15013, .F. ) ;
#10795=CIRCLE ( 'NONE', #19970, 5.499999999999998224 ) ;
#10806=ADVANCED_FACE ( 'NONE', ( #451 ), #16441, .F. ) ;
#10833=EDGE_CURVE ( 'NONE', #47191, #371, #44098, .T. ) ;
#10844=VERTEX_POINT ( 'NONE', #5944 ) ;
#10855=LINE ( 'NONE', #23136, #45678 ) ;
#10884=ORIENTED_EDGE ( 'NONE', *, *, #44385, .F. ) ;
#10885=FACE_OUTER_BOUND ( 'NONE', #32887, .T. ) ;
#10900=ORIENTED_EDGE ( 'NONE', *, *, #25246, .F. ) ;
#10905=CIRCLE ( 'NONE', #22586, 19.50000000000000000 ) ;
#10909=AXIS2_PLACEMENT_3D ( 'NONE', #48589, #21040, #881 ) ;
#10914=CARTESIAN_POINT ( 'NONE',  ( 16.13393739769620083, -15.61618894467929941, 9.349999999999999645 ) ) ;
#10933=ADVANCED_FACE ( 'NONE', ( #34477 ), #23168, .T. ) ;
#10941=DIRECTION ( 'NONE',  ( 1.000000000000000000, 0.000000000000000000, 0.000000000000000000 ) ) ;
#11019=TOROIDAL_SURFACE ( 'NONE', #37764, 36.50000000076989437, 1.500000000038270054 ) ;
#11023=ORIENTED_EDGE ( 'NONE', *, *, #15135, .T. ) ;
#11039=VERTEX_POINT ( 'NONE', #22297 ) ;
#11050=AXIS2_PLACEMENT_3D ( 'NONE', #12862, #33528, #1052 ) ;
#11060=LINE ( 'NONE', #18387, #38050 ) ;
#11069=CARTESIAN_POINT ( 'NONE',  ( 51.13393739769620083, 19.38381105532069881, 17.35000000000000142 ) ) ;
#11071=EDGE_CURVE ( 'NONE', #12691, #51462, #5621, .T. ) ;
#11089=DIRECTION ( 'NONE',  ( 0.7071067811865470176, -8.659560562354926695E-17, 0.7071067811865480168 ) ) ;
#11094=DIRECTION ( 'NONE',  ( 1.000000000000000000, 0.000000000000000000, 0.000000000000000000 ) ) ;
#11095=AXIS2_PLACEMENT_3D ( 'NONE', #31606, #15650, #38993 ) ;
#11113=CARTESIAN_POINT ( 'NONE',  ( 29.63393739769620083, -15.61618894467929941, -1.149999999999999911 ) ) ;
#11125=CIRCLE ( 'NONE', #51262, 1.000000000000000000 ) ;
#11148=VERTEX_POINT ( 'NONE', #10270 ) ;
#11161=CIRCLE ( 'NONE', #15348, 5.999999999999998224 ) ;
#11195=TOROIDAL_SURFACE ( 'NONE', #24543, 17.07000000028409659, 3.569999999987189643 ) ;
#11201=DIRECTION ( 'NONE',  ( 1.000000000000000000, -1.703274131079987031E-27, 2.066387465239710029E-12 ) ) ;
#11206=EDGE_LOOP ( 'NONE', ( #9996, #1617 ) ) ;
#11214=ORIENTED_EDGE ( 'NONE', *, *, #20724, .T. ) ;
#11232=DIRECTION ( 'NONE',  ( 0.000000000000000000, 0.000000000000000000, -1.000000000000000000 ) ) ;
#11233=ADVANCED_FACE ( 'NONE', ( #17044, #28815 ), #44816, .T. ) ;
#11236=CIRCLE ( 'NONE', #26246, 1.000000000000000888 ) ;
#11246=DIRECTION ( 'NONE',  ( -0.7071067811865476838, -0.7071067811865473507, 0.000000000000000000 ) ) ;
#11263=AXIS2_PLACEMENT_3D ( 'NONE', #36884, #21145, #40558 ) ;
#11288=ORIENTED_EDGE ( 'NONE', *, *, #17434, .F. ) ;
#11289=CARTESIAN_POINT ( 'NONE',  ( 25.90218739769619916, -15.61618894467930119, -18.08174999999999955 ) ) ;
#11294=VECTOR ( 'NONE', #41379, 1000.000000000000000 ) ;
#11307=DIRECTION ( 'NONE',  ( 0.000000000000000000, 3.858025010473989332E-12, 1.000000000000000000 ) ) ;
#11319=FACE_OUTER_BOUND ( 'NONE', #1971, .T. ) ;
#11320=CARTESIAN_POINT ( 'NONE',  ( -18.86606260230390220, 19.38381105532060289, 16.21999999999999886 ) ) ;
#11351=ORIENTED_EDGE ( 'NONE', *, *, #25299, .T. ) ;
#11382=DIRECTION ( 'NONE',  ( 0.000000000000000000, 0.000000000000000000, 1.000000000000000000 ) ) ;
#11406=VECTOR ( 'NONE', #18836, 1000.000000000000000 ) ;
#11421=DIRECTION ( 'NONE',  ( 0.000000000000000000, 0.000000000000000000, 1.000000000000000000 ) ) ;
#11427=AXIS2_PLACEMENT_3D ( 'NONE', #25859, #9650, #46600 ) ;
#11431=DIRECTION ( 'NONE',  ( 1.000000000000000000, 8.701345253104295327E-30, 2.840828347717470042E-11 ) ) ;
#11440=CIRCLE ( 'NONE', #6424, 0.4999999999856508115 ) ;
#11457=ORIENTED_EDGE ( 'NONE', *, *, #29038, .T. ) ;
#11468=ORIENTED_EDGE ( 'NONE', *, *, #36349, .T. ) ;
#11478=ORIENTED_EDGE ( 'NONE', *, *, #50164, .T. ) ;
#11496=DIRECTION ( 'NONE',  ( 0.000000000000000000, 0.000000000000000000, -1.000000000000000000 ) ) ;
#11563=DIRECTION ( 'NONE',  ( -1.000000000000000000, 0.000000000000000000, 0.000000000000000000 ) ) ;
#11588=CARTESIAN_POINT ( 'NONE',  ( 16.13393739769620083, -15.61618894467929941, -8.849999999999999645 ) ) ;
#11590=EDGE_CURVE ( 'NONE', #31235, #6972, #51823, .T. ) ;
#11617=ADVANCED_FACE ( 'NONE', ( #10090 ), #26747, .F. ) ;
#11626=AXIS2_PLACEMENT_3D ( 'NONE', #8687, #36980, #20206 ) ;
#11635=DIRECTION ( 'NONE',  ( 1.000000000000000000, 0.000000000000000000, 0.000000000000000000 ) ) ;
#11644=DIRECTION ( 'NONE',  ( 0.000000000000000000, 0.7071067811865457964, 0.7071067811865492381 ) ) ;
#11646=CARTESIAN_POINT ( 'NONE',  ( 63.63393739769619373, -53.11618894467930119, 11.84999999999999964 ) ) ;
#11648=EDGE_CURVE ( 'NONE', #42921, #17993, #40155, .T. ) ;
#11663=ORIENTED_EDGE ( 'NONE', *, *, #50105, .F. ) ;
#11665=ORIENTED_EDGE ( 'NONE', *, *, #33909, .F. ) ;
#11693=CYLINDRICAL_SURFACE ( 'NONE', #19634, 0.9999999999999988898 ) ;
#11704=EDGE_CURVE ( 'NONE', #50005, #41343, #4035, .T. ) ;
#11721=ORIENTED_EDGE ( 'NONE', *, *, #45388, .F. ) ;
#11735=AXIS2_PLACEMENT_3D ( 'NONE', #27695, #8047, #23746 ) ;
#11747=FACE_OUTER_BOUND ( 'NONE', #37510, .T. ) ;
#11762=DIRECTION ( 'NONE',  ( 1.000000000000000000, 0.000000000000000000, 0.000000000000000000 ) ) ;
#11763=CIRCLE ( 'NONE', #52, 13.50000000000000000 ) ;
#11773=DIRECTION ( 'NONE',  ( 0.000000000000000000, 0.000000000000000000, 1.000000000000000000 ) ) ;
#11788=CARTESIAN_POINT ( 'NONE',  ( -21.36606260230379917, -53.11618894467930119, 17.35000000000000142 ) ) ;
#11791=ORIENTED_EDGE ( 'NONE', *, *, #352, .T. ) ;
#11802=ORIENTED_EDGE ( 'NONE', *, *, #24326, .T. ) ;
#11806=DIRECTION ( 'NONE',  ( 0.000000000000000000, 0.000000000000000000, 1.000000000000000000 ) ) ;
#11810=AXIS2_PLACEMENT_3D ( 'NONE', #47862, #3838, #19812 ) ;
#11813=AXIS2_PLACEMENT_3D ( 'NONE', #16756, #255, #12573 ) ;
#11823=CYLINDRICAL_SURFACE ( 'NONE', #1938, 0.9999999999999988898 ) ;
#11826=DIRECTION ( 'NONE',  ( 1.000000000000000000, 0.000000000000000000, 0.000000000000000000 ) ) ;
#11840=ORIENTED_EDGE ( 'NONE', *, *, #41839, .T. ) ;
#11851=ADVANCED_FACE ( 'NONE', ( #9780 ), #46470, .F. ) ;
#11873=CARTESIAN_POINT ( 'NONE',  ( 53.63393739769619373, 21.88381105532059934, 16.35000000000000142 ) ) ;
#11900=DIRECTION ( 'NONE',  ( 0.000000000000000000, 0.000000000000000000, -1.000000000000000000 ) ) ;
#11901=VERTEX_POINT ( 'NONE', #17889 ) ;
#11928=ORIENTED_EDGE ( 'NONE', *, *, #10408, .F. ) ;
#11930=CARTESIAN_POINT ( 'NONE',  ( -31.07316938349034885, 8.133811055320650851, 17.05710678118654755 ) ) ;
#11946=AXIS2_PLACEMENT_3D ( 'NONE', #36860, #4625, #32640 ) ;
#11953=CARTESIAN_POINT ( 'NONE',  ( 62.63393739769619373, -39.36618894467940066, 16.35000000000000142 ) ) ;
#11972=CARTESIAN_POINT ( 'NONE',  ( 20.78393739769619941, -15.61618894467929941, -9.721247897589949005 ) ) ;
#11992=CARTESIAN_POINT ( 'NONE',  ( 46.68434392863400717, 16.15099216771209001, 16.85000000000000142 ) ) ;
#11996=ORIENTED_EDGE ( 'NONE', *, *, #29368, .T. ) ;
#12009=EDGE_CURVE ( 'NONE', #1350, #10341, #3303, .T. ) ;
#12018=CIRCLE ( 'NONE', #49698, 18.86180339887500068 ) ;
#12020=AXIS2_PLACEMENT_3D ( 'NONE', #36200, #310, #47762 ) ;
#12183=ORIENTED_EDGE ( 'NONE', *, *, #47577, .T. ) ;
#12224=DIRECTION ( 'NONE',  ( 1.000000000000000000, 0.000000000000000000, 0.000000000000000000 ) ) ;
#12231=ORIENTED_EDGE ( 'NONE', *, *, #29835, .T. ) ;
#12236=AXIS2_PLACEMENT_3D ( 'NONE', #26675, #21710, #17797 ) ;
#12237=ORIENTED_EDGE ( 'NONE', *, *, #45414, .F. ) ;
#12244=DIRECTION ( 'NONE',  ( 0.000000000000000000, 1.000000000000000000, 0.000000000000000000 ) ) ;
#12245=ADVANCED_FACE ( 'NONE', ( #26904 ), #50767, .T. ) ;
#12255=CIRCLE ( 'NONE', #526, 10.00000000000000888 ) ;
#12261=DIRECTION ( 'NONE',  ( -1.000000000000000000, 0.000000000000000000, 0.000000000000000000 ) ) ;
#12281=VERTEX_POINT ( 'NONE', #18986 ) ;
#12313=PLANE ( 'NONE',  #43478 ) ;
#12323=VECTOR ( 'NONE', #4943, 999.9999999999998863 ) ;
#12341=CYLINDRICAL_SURFACE ( 'NONE', #26860, 13.50000000000000178 ) ;
#12392=ORIENTED_EDGE ( 'NONE', *, *, #1568, .T. ) ;
#12431=ORIENTED_EDGE ( 'NONE', *, *, #4320, .T. ) ;
#12433=CARTESIAN_POINT ( 'NONE',  ( 51.13393739769659874, -50.61618894467899565, 10.84999999999999964 ) ) ;
#12459=AXIS2_PLACEMENT_3D ( 'NONE', #16688, #40794, #37128 ) ;
#12487=CARTESIAN_POINT ( 'NONE',  ( -18.86606260230360022, -50.61618894467959962, 11.34999999999999964 ) ) ;
#12509=AXIS2_PLACEMENT_3D ( 'NONE', #28056, #51165, #35687 ) ;
#12512=DIRECTION ( 'NONE',  ( 0.000000000000000000, 0.000000000000000000, 1.000000000000000000 ) ) ;
#12513=AXIS2_PLACEMENT_3D ( 'NONE', #31030, #20263, #3271 ) ;
#12535=DIRECTION ( 'NONE',  ( 0.000000000000000000, 0.000000000000000000, 1.000000000000000000 ) ) ;
#12543=CARTESIAN_POINT ( 'NONE',  ( -23.31565607136580098, -47.38337005707097660, 11.34999999999999964 ) ) ;
#12573=DIRECTION ( 'NONE',  ( 0.000000000000000000, 1.000000000000000000, 0.000000000000000000 ) ) ;
#12583=CIRCLE ( 'NONE', #48566, 11.00000000000000000 ) ;
#12600=CIRCLE ( 'NONE', #29681, 9.000000000000007105 ) ;
#12638=ORIENTED_EDGE ( 'NONE', *, *, #5162, .T. ) ;
#12643=CARTESIAN_POINT ( 'NONE',  ( 16.13393739769620083, -15.61618894467929941, 9.349999999999999645 ) ) ;
#12676=DIRECTION ( 'NONE',  ( 1.000000000000000000, 0.000000000000000000, 0.000000000000000000 ) ) ;
#12691=VERTEX_POINT ( 'NONE', #5086 ) ;
#12701=VERTEX_POINT ( 'NONE', #21039 ) ;
#12743=FACE_OUTER_BOUND ( 'NONE', #3542, .T. ) ;
#12762=ORIENTED_EDGE ( 'NONE', *, *, #4835, .F. ) ;
#12768=LINE ( 'NONE', #32125, #45966 ) ;
#12785=EDGE_CURVE ( 'NONE', #34913, #3068, #18413, .T. ) ;
#12795=DIRECTION ( 'NONE',  ( 0.000000000000000000, 0.000000000000000000, 1.000000000000000000 ) ) ;
#12803=CARTESIAN_POINT ( 'NONE',  ( 35.44295439207109411, -15.61618894467929941, 17.35000000000000142 ) ) ;
#12806=CIRCLE ( 'NONE', #3751, 9.000000000000007105 ) ;
#12807=VECTOR ( 'NONE', #2351, 1000.000000000000000 ) ;
#12819=ORIENTED_EDGE ( 'NONE', *, *, #7344, .F. ) ;
#12825=DIRECTION ( 'NONE',  ( 0.000000000000000000, -0.7071067811865492381, -0.7071067811865457964 ) ) ;
#12848=CIRCLE ( 'NONE', #10298, 9.768249999999998323 ) ;
#12850=AXIS2_PLACEMENT_3D ( 'NONE', #37694, #49759, #29809 ) ;
#12852=DIRECTION ( 'NONE',  ( 0.000000000000000000, -1.000000000000000000, 0.000000000000000000 ) ) ;
#12862=CARTESIAN_POINT ( 'NONE',  ( 16.13393739769620083, -15.61618894467929941, 9.349999999999999645 ) ) ;
#12895=ORIENTED_EDGE ( 'NONE', *, *, #36257, .T. ) ;
#12896=ORIENTED_EDGE ( 'NONE', *, *, #20724, .F. ) ;
#12900=ORIENTED_EDGE ( 'NONE', *, *, #36077, .F. ) ;
#12902=CARTESIAN_POINT ( 'NONE',  ( 51.13393739769659874, -56.11618894467899565, 11.34999999999999964 ) ) ;
#12939=CARTESIAN_POINT ( 'NONE',  ( 6.383937397696199945, -15.61618894467929941, -18.10000000000000142 ) ) ;
#12957=VERTEX_POINT ( 'NONE', #30841 ) ;
#12959=AXIS2_PLACEMENT_3D ( 'NONE', #27150, #43157, #23456 ) ;
#12960=ORIENTED_EDGE ( 'NONE', *, *, #24191, .F. ) ;
#12962=CARTESIAN_POINT ( 'NONE',  ( -30.36606260230379917, -53.11618894467940066, 17.35000000000000142 ) ) ;
#12964=EDGE_CURVE ( 'NONE', #8804, #24630, #6719, .T. ) ;
#12975=ORIENTED_EDGE ( 'NONE', *, *, #30582, .F. ) ;
#12987=CARTESIAN_POINT ( 'NONE',  ( -18.86606260230360022, -50.61618894467959962, 10.84999999999999964 ) ) ;
#13015=DIRECTION ( 'NONE',  ( 0.000000000000000000, 0.000000000000000000, -1.000000000000000000 ) ) ;
#13022=VERTEX_POINT ( 'NONE', #44722 ) ;
#13032=FACE_BOUND ( 'NONE', #44140, .T. ) ;
#13035=DIRECTION ( 'NONE',  ( -1.000000000000000000, 0.000000000000000000, 0.000000000000000000 ) ) ;
#13037=DIRECTION ( 'NONE',  ( -1.000000000000000000, 0.000000000000000000, 0.000000000000000000 ) ) ;
#13048=ADVANCED_FACE ( 'NONE', ( #42290 ), #29237, .T. ) ;
#13054=TOROIDAL_SURFACE ( 'NONE', #20532, 12.50000000000000000, 1.000000000000000000 ) ;
#13072=DIRECTION ( 'NONE',  ( 0.000000000000000000, 0.000000000000000000, 1.000000000000000000 ) ) ;
#13078=CARTESIAN_POINT ( 'NONE',  ( -20.36606260370279742, -15.61618894417470571, 10.84999999934590242 ) ) ;
#13093=CARTESIAN_POINT ( 'NONE',  ( 50.62425669123998517, 19.75411576426495586, 16.21999999999999886 ) ) ;
#13097=AXIS2_PLACEMENT_3D ( 'NONE', #36950, #16514, #24353 ) ;
#13099=ADVANCED_FACE ( 'NONE', ( #6910, #34660, #18427, #42814, #13032, #6130 ), #17208, .T. ) ;
#13107=CARTESIAN_POINT ( 'NONE',  ( 26.13393739769619728, -15.61618894467929941, -18.35000000000000142 ) ) ;
#13108=DIRECTION ( 'NONE',  ( 0.000000000000000000, 0.000000000000000000, -1.000000000000000000 ) ) ;
#13110=CARTESIAN_POINT ( 'NONE',  ( 63.63393739769619373, 21.88381105532059934, 16.35000000000000142 ) ) ;
#13111=CARTESIAN_POINT ( 'NONE',  ( 28.63393739769620083, -15.61618894467929941, -1.149999999999999911 ) ) ;
#13136=ORIENTED_EDGE ( 'NONE', *, *, #35368, .T. ) ;
#13150=EDGE_LOOP ( 'NONE', ( #17622, #49241, #11478, #40554, #11468 ) ) ;
#13157=CARTESIAN_POINT ( 'NONE',  ( 51.50424210664085223, -50.10650823822277289, 16.21999999999999886 ) ) ;
#13164=ORIENTED_EDGE ( 'NONE', *, *, #39535, .T. ) ;
#13176=CIRCLE ( 'NONE', #8135, 18.00000000000000000 ) ;
#13192=EDGE_CURVE ( 'NONE', #25606, #27172, #49446, .T. ) ;
#13196=CARTESIAN_POINT ( 'NONE',  ( 16.13393739769620083, -15.61618894467929941, 14.34999999999999964 ) ) ;
#13213=DIRECTION ( 'NONE',  ( 1.000000000000000000, 0.000000000000000000, 0.000000000000000000 ) ) ;
#13217=ORIENTED_EDGE ( 'NONE', *, *, #33459, .T. ) ;
#13231=DIRECTION ( 'NONE',  ( 0.000000000000000000, 0.000000000000000000, -1.000000000000000000 ) ) ;
#13281=DIRECTION ( 'NONE',  ( 1.000000000000000000, 0.000000000000000000, 0.000000000000000000 ) ) ;
#13323=ORIENTED_EDGE ( 'NONE', *, *, #27679, .F. ) ;
#13343=AXIS2_PLACEMENT_3D ( 'NONE', #32076, #28153, #44157 ) ;
#13346=DIRECTION ( 'NONE',  ( 0.000000000000000000, 0.000000000000000000, 1.000000000000000000 ) ) ;
#13366=CARTESIAN_POINT ( 'NONE',  ( 46.27983543144653567, 22.91052256907554607, 10.84999999999999964 ) ) ;
#13372=AXIS2_PLACEMENT_3D ( 'NONE', #28535, #33242, #40597 ) ;
#13375=AXIS2_PLACEMENT_3D ( 'NONE', #46002, #3004, #34956 ) ;
#13409=ORIENTED_EDGE ( 'NONE', *, *, #18378, .T. ) ;
#13413=AXIS2_PLACEMENT_3D ( 'NONE', #37658, #46577, #50240 ) ;
#13427=ADVANCED_FACE ( 'NONE', ( #49066 ), #36854, .F. ) ;
#13439=CIRCLE ( 'NONE', #38, 5.999999999999998224 ) ;
#13455=CARTESIAN_POINT ( 'NONE',  ( -24.36606260230359666, -50.61618894467959962, 16.85000000000000142 ) ) ;
#13458=VECTOR ( 'NONE', #22286, 1000.000000000000000 ) ;
#13490=DIRECTION ( 'NONE',  ( -0.5720614028176865817, -0.4156269377774495233, 0.7071067811865480168 ) ) ;
#13493=VERTEX_POINT ( 'NONE', #24393 ) ;
#13519=ORIENTED_EDGE ( 'NONE', *, *, #37335, .T. ) ;
#13540=ORIENTED_EDGE ( 'NONE', *, *, #35259, .T. ) ;
#13557=CIRCLE ( 'NONE', #45350, 13.00000000000000178 ) ;
#13564=EDGE_CURVE ( 'NONE', #39558, #48021, #2653, .T. ) ;
#13595=VERTEX_POINT ( 'NONE', #18357 ) ;
#13598=ADVANCED_FACE ( 'NONE', ( #2131, #34601, #46689, #22543, #29884, #14438 ), #34336, .T. ) ;
#13604=VERTEX_POINT ( 'NONE', #46430 ) ;
#13610=DIRECTION ( 'NONE',  ( 0.000000000000000000, 0.000000000000000000, -1.000000000000000000 ) ) ;
#13620=EDGE_CURVE ( 'NONE', #44905, #6898, #30059, .T. ) ;
#13641=EDGE_CURVE ( 'NONE', #42293, #41355, #6066, .T. ) ;
#13676=CARTESIAN_POINT ( 'NONE',  ( -24.36606260230359666, -50.61618894467959962, 14.21249999999999858 ) ) ;
#13731=ORIENTED_EDGE ( 'NONE', *, *, #6270, .T. ) ;
#13734=DIRECTION ( 'NONE',  ( 0.000000000000000000, 0.000000000000000000, 1.000000000000000000 ) ) ;
#13735=EDGE_CURVE ( 'NONE', #16294, #44712, #37590, .T. ) ;
#13741=VERTEX_POINT ( 'NONE', #38820 ) ;
#13743=DIRECTION ( 'NONE',  ( -1.000000000000000000, 0.000000000000000000, 0.000000000000000000 ) ) ;
#13757=VECTOR ( 'NONE', #19207, 1000.000000000000114 ) ;
#13772=ORIENTED_EDGE ( 'NONE', *, *, #44316, .F. ) ;
#13786=ORIENTED_EDGE ( 'NONE', *, *, #9053, .F. ) ;
#13795=CIRCLE ( 'NONE', #34723, 19.30901699437490038 ) ;
#13798=CARTESIAN_POINT ( 'NONE',  ( 56.63393739769620083, 19.38381105532069881, 11.34999999999999964 ) ) ;
#13814=DIRECTION ( 'NONE',  ( 5.878706999999999976E-17, 3.795112000000000086E-17, 1.000000000000000000 ) ) ;
#13827=ORIENTED_EDGE ( 'NONE', *, *, #9804, .F. ) ;
#13836=FACE_OUTER_BOUND ( 'NONE', #33049, .T. ) ;
#13838=DIRECTION ( 'NONE',  ( 0.7071067811865475727, 0.7071067811865475727, 0.000000000000000000 ) ) ;
#13854=CARTESIAN_POINT ( 'NONE',  ( -21.36606260230379917, 30.88381105532059934, 11.84999999999999964 ) ) ;
#13857=ORIENTED_EDGE ( 'NONE', *, *, #16254, .T. ) ;
#13865=CIRCLE ( 'NONE', #31418, 0.9999999999999940048 ) ;
#13874=FACE_OUTER_BOUND ( 'NONE', #21537, .T. ) ;
#13880=CARTESIAN_POINT ( 'NONE',  ( 15.61576201279904552, -15.99266539877262971, -12.13039854958090125 ) ) ;
#13900=CARTESIAN_POINT ( 'NONE',  ( 16.13393739769620083, -15.61618894467929941, 17.35000000000000142 ) ) ;
#13903=EDGE_LOOP ( 'NONE', ( #1712, #3435, #16362, #4551 ) ) ;
#13921=ADVANCED_FACE ( 'NONE', ( #4697 ), #31742, .T. ) ;
#13929=AXIS2_PLACEMENT_3D ( 'NONE', #5717, #21673, #13838 ) ;
#13933=CIRCLE ( 'NONE', #43222, 0.9999999999999940048 ) ;
#13983=DIRECTION ( 'NONE',  ( 0.6934629132905124616, 0.5038302981000506442, 0.5150380749100490485 ) ) ;
#13985=ORIENTED_EDGE ( 'NONE', *, *, #14940, .T. ) ;
#13986=ADVANCED_FACE ( 'NONE', ( #5234 ), #45994, .F. ) ;
#14024=CARTESIAN_POINT ( 'NONE',  ( 11.48393739769620048, -15.61618894467929941, -18.35000000000000142 ) ) ;
#14055=ADVANCED_FACE ( 'NONE', ( #32976, #49001 ), #12313, .T. ) ;
#14071=DIRECTION ( 'NONE',  ( -0.7071067811865475727, 0.000000000000000000, 0.7071067811865475727 ) ) ;
#14083=DIRECTION ( 'NONE',  ( 0.000000000000000000, 0.000000000000000000, -1.000000000000000000 ) ) ;
#14091=CARTESIAN_POINT ( 'NONE',  ( 26.13393739769619728, -15.61618894467929941, -5.966499999999999915 ) ) ;
#14117=EDGE_CURVE ( 'NONE', #48021, #12701, #40964, .T. ) ;
#14134=DIRECTION ( 'NONE',  ( 0.000000000000000000, 0.000000000000000000, 1.000000000000000000 ) ) ;
#14145=ORIENTED_EDGE ( 'NONE', *, *, #30165, .T. ) ;
#14165=LINE ( 'NONE', #1857, #48540 ) ;
#14178=ORIENTED_EDGE ( 'NONE', *, *, #704, .T. ) ;
#14181=CARTESIAN_POINT ( 'NONE',  ( 53.63393739769619373, 31.88381105532059934, 11.84999999999999964 ) ) ;
#14184=ADVANCED_FACE ( 'NONE', ( #11747 ), #35834, .T. ) ;
#14208=CARTESIAN_POINT ( 'NONE',  ( 53.63393739769619373, 30.88381105532059934, 10.84999999999999964 ) ) ;
#14218=DIRECTION ( 'NONE',  ( 0.000000000000000000, -1.000000000000000000, 0.000000000000000000 ) ) ;
#14219=DIRECTION ( 'NONE',  ( 1.062456999999999985E-16, -7.719205000000000365E-17, 1.000000000000000000 ) ) ;
#14236=ORIENTED_EDGE ( 'NONE', *, *, #4320, .F. ) ;
#14243=CARTESIAN_POINT ( 'NONE',  ( 51.13393739769659874, -50.61618894467899565, 11.34999999999999964 ) ) ;
#14245=ORIENTED_EDGE ( 'NONE', *, *, #42591, .F. ) ;
#14254=EDGE_CURVE ( 'NONE', #29295, #7519, #46033, .T. ) ;
#14269=ORIENTED_EDGE ( 'NONE', *, *, #40321, .T. ) ;
#14338=VERTEX_POINT ( 'NONE', #44473 ) ;
#14350=DIRECTION ( 'NONE',  ( 0.000000000000000000, 0.000000000000000000, 1.000000000000000000 ) ) ;
#14378=EDGE_CURVE ( 'NONE', #25374, #10844, #36536, .T. ) ;
#14403=AXIS2_PLACEMENT_3D ( 'NONE', #25603, #14350, #22712 ) ;
#14417=EDGE_CURVE ( 'NONE', #9032, #16350, #48531, .T. ) ;
#14438=FACE_OUTER_BOUND ( 'NONE', #23807, .T. ) ;
#14449=CIRCLE ( 'NONE', #34522, 3.569999999999939444 ) ;
#14462=DIRECTION ( 'NONE',  ( 0.000000000000000000, 0.000000000000000000, 1.000000000000000000 ) ) ;
#14474=DIRECTION ( 'NONE',  ( 0.7071067811865475727, -0.7071067811865475727, 0.000000000000000000 ) ) ;
#14488=ORIENTED_EDGE ( 'NONE', *, *, #32904, .T. ) ;
#14490=VERTEX_POINT ( 'NONE', #32844 ) ;
#14491=ORIENTED_EDGE ( 'NONE', *, *, #36357, .F. ) ;
#14502=LINE ( 'NONE', #26283, #44376 ) ;
#14507=CIRCLE ( 'NONE', #43788, 18.86180339887500068 ) ;
#14517=DIRECTION ( 'NONE',  ( 0.000000000000000000, 0.000000000000000000, -1.000000000000000000 ) ) ;
#14526=CARTESIAN_POINT ( 'NONE',  ( 16.13393739769620083, -15.61618894467929941, 16.85000000000000142 ) ) ;
#14529=CARTESIAN_POINT ( 'NONE',  ( 8.231257142393115345, -9.874555653973354552, -18.08174999999999955 ) ) ;
#14562=AXIS2_PLACEMENT_3D ( 'NONE', #26953, #31899, #23777 ) ;
#14565=CARTESIAN_POINT ( 'NONE',  ( -18.86606260230360022, -50.61618894467959962, 14.21249999999999858 ) ) ;
#14566=EDGE_CURVE ( 'NONE', #19834, #23063, #31776, .T. ) ;
#14573=VECTOR ( 'NONE', #48998, 1000.000000000000000 ) ;
#14592=EDGE_CURVE ( 'NONE', #44136, #45507, #19598, .T. ) ;
#14601=DIRECTION ( 'NONE',  ( -1.000000000000000000, 0.000000000000000000, 0.000000000000000000 ) ) ;
#14607=EDGE_CURVE ( 'NONE', #23688, #51520, #2854, .T. ) ;
#14609=DIRECTION ( 'NONE',  ( -2.619602780254359830E-11, 3.858400438143729530E-12, 1.000000000000000000 ) ) ;
#14611=CARTESIAN_POINT ( 'NONE',  ( 51.13393739769659874, -50.61618894467899565, 14.21249999999999858 ) ) ;
#14612=ORIENTED_EDGE ( 'NONE', *, *, #19023, .F. ) ;
#14626=EDGE_CURVE ( 'NONE', #20497, #23063, #10905, .T. ) ;
#14655=DIRECTION ( 'NONE',  ( 1.000000000000000000, 1.222653822078627158E-29, -4.718060457820110146E-11 ) ) ;
#14670=EDGE_CURVE ( 'NONE', #28389, #4191, #28415, .T. ) ;
#14710=EDGE_CURVE ( 'NONE', #18163, #47819, #23248, .T. ) ;
#14725=DIRECTION ( 'NONE',  ( -1.000000000000000000, 0.000000000000000000, 0.000000000000000000 ) ) ;
#14732=CARTESIAN_POINT ( 'NONE',  ( -21.36606260230379917, -62.82329572586585442, 11.14289321881345529 ) ) ;
#14748=AXIS2_PLACEMENT_3D ( 'NONE', #30696, #46718, #18651 ) ;
#14761=DIRECTION ( 'NONE',  ( 0.000000000000000000, 1.000000000000000000, 0.000000000000000000 ) ) ;
#14767=VECTOR ( 'NONE', #46074, 1000.000000000000000 ) ;
#14775=EDGE_CURVE ( 'NONE', #27489, #19246, #36803, .T. ) ;
#14794=EDGE_CURVE ( 'NONE', #11039, #42293, #17552, .T. ) ;
#14796=AXIS2_PLACEMENT_3D ( 'NONE', #29994, #49433, #10107 ) ;
#14822=ORIENTED_EDGE ( 'NONE', *, *, #49923, .T. ) ;
#14839=DIRECTION ( 'NONE',  ( -1.000000000000000000, 0.000000000000000000, 0.000000000000000000 ) ) ;
#14856=ORIENTED_EDGE ( 'NONE', *, *, #45978, .T. ) ;
#14885=CARTESIAN_POINT ( 'NONE',  ( -18.86606260230360022, -50.61618894467959962, 16.85000000000000142 ) ) ;
#14898=AXIS2_PLACEMENT_3D ( 'NONE', #28491, #51840, #11762 ) ;
#14917=ADVANCED_FACE ( 'NONE', ( #25052 ), #47750, .T. ) ;
#14925=CARTESIAN_POINT ( 'NONE',  ( 51.13393739769659874, -56.11618894467899565, 16.85000000000000142 ) ) ;
#14938=CARTESIAN_POINT ( 'NONE',  ( 51.13393739769620083, 19.38381105532069881, 11.34999999999999964 ) ) ;
#14940=EDGE_CURVE ( 'NONE', #2702, #29187, #25123, .T. ) ;
#14982=ORIENTED_EDGE ( 'NONE', *, *, #51280, .F. ) ;
#15013=EDGE_CURVE ( 'NONE', #18163, #1900, #46066, .T. ) ;
#15016=CARTESIAN_POINT ( 'NONE',  ( 47.90111851008803967, -55.06578241374122484, 11.34999999999999964 ) ) ;
#15029=CYLINDRICAL_SURFACE ( 'NONE', #30885, 0.9999999999999988898 ) ;
#15042=AXIS2_PLACEMENT_3D ( 'NONE', #17748, #28759, #49483 ) ;
#15055=CIRCLE ( 'NONE', #4992, 0.4999999999856508115 ) ;
#15062=LINE ( 'NONE', #2756, #8360 ) ;
#15073=ORIENTED_EDGE ( 'NONE', *, *, #33575, .T. ) ;
#15083=CIRCLE ( 'NONE', #44366, 19.50000000000000000 ) ;
#15124=DIRECTION ( 'NONE',  ( 0.000000000000000000, 0.000000000000000000, 1.000000000000000000 ) ) ;
#15128=AXIS2_PLACEMENT_3D ( 'NONE', #18279, #33993, #45301 ) ;
#15135=EDGE_CURVE ( 'NONE', #17657, #46911, #48563, .T. ) ;
#15141=ORIENTED_EDGE ( 'NONE', *, *, #17798, .T. ) ;
#15151=CARTESIAN_POINT ( 'NONE',  ( 16.13393739767329649, -15.61618894439989980, -19.08999999984770213 ) ) ;
#15279=AXIS2_PLACEMENT_3D ( 'NONE', #46750, #6904, #11094 ) ;
#15291=DIRECTION ( 'NONE',  ( 0.000000000000000000, 0.7071067811865457964, -0.7071067811865492381 ) ) ;
#15336=ORIENTED_EDGE ( 'NONE', *, *, #35357, .T. ) ;
#15339=DIRECTION ( 'NONE',  ( 0.000000000000000000, 0.000000000000000000, 1.000000000000000000 ) ) ;
#15348=AXIS2_PLACEMENT_3D ( 'NONE', #46462, #3199, #18909 ) ;
#15363=ADVANCED_FACE ( 'NONE', ( #8628 ), #49442, .F. ) ;
#15378=AXIS2_PLACEMENT_3D ( 'NONE', #46070, #5968, #41601 ) ;
#15391=EDGE_LOOP ( 'NONE', ( #46816, #18868, #37892, #20538 ) ) ;
#15414=CARTESIAN_POINT ( 'NONE',  ( 31.39345689194515643, -4.529499075180571488, 17.07360679774999923 ) ) ;
#15420=DIRECTION ( 'NONE',  ( 1.224646799147353207E-16, 1.000000000000000000, -0.000000000000000000 ) ) ;
#15423=VECTOR ( 'NONE', #40248, 1000.000000000000000 ) ;
#15443=VERTEX_POINT ( 'NONE', #48461 ) ;
#15470=EDGE_LOOP ( 'NONE', ( #18261, #32977, #36908, #34018 ) ) ;
#15480=CIRCLE ( 'NONE', #28023, 1.500000000038269388 ) ;
#15493=CARTESIAN_POINT ( 'NONE',  ( 16.13393739769620083, -15.61618894467929941, 17.35000000000000142 ) ) ;
#15520=AXIS2_PLACEMENT_3D ( 'NONE', #79, #47018, #19467 ) ;
#15574=CARTESIAN_POINT ( 'NONE',  ( -21.36606260230379917, 31.88381105532059934, 11.84999999999999964 ) ) ;
#15595=AXIS2_PLACEMENT_3D ( 'NONE', #11873, #7677, #47513 ) ;
#15616=VECTOR ( 'NONE', #5197, 1000.000000000000000 ) ;
#15627=DIRECTION ( 'NONE',  ( 0.000000000000000000, 0.000000000000000000, 1.000000000000000000 ) ) ;
#15648=ORIENTED_EDGE ( 'NONE', *, *, #8148, .F. ) ;
#15650=DIRECTION ( 'NONE',  ( 0.000000000000000000, 0.000000000000000000, 1.000000000000000000 ) ) ;
#15654=AXIS2_PLACEMENT_3D ( 'NONE', #22770, #34571, #2881 ) ;
#15669=CARTESIAN_POINT ( 'NONE',  ( 16.13393739769620083, -15.61618894467929941, -18.58999999999999986 ) ) ;
#15677=CARTESIAN_POINT ( 'NONE',  ( -7.616062602303800055, -62.11618894467930119, 16.35000000000000142 ) ) ;
#15696=ORIENTED_EDGE ( 'NONE', *, *, #14670, .F. ) ;
#15724=CARTESIAN_POINT ( 'NONE',  ( 60.70500520956167634, -60.18725675654477669, 17.35000000000000142 ) ) ;
#15739=CARTESIAN_POINT ( 'NONE',  ( 16.13393739769620083, -15.61618894467929941, 14.34999999999999964 ) ) ;
#15740=DIRECTION ( 'NONE',  ( 0.000000000000000000, 0.000000000000000000, -1.000000000000000000 ) ) ;
#15744=CARTESIAN_POINT ( 'NONE',  ( 16.13393739769620083, -15.61618894467929941, -5.966499999999999915 ) ) ;
#15745=DIRECTION ( 'NONE',  ( 0.8090169943749462300, -0.5877852522924749135, 0.000000000000000000 ) ) ;
#15765=DIRECTION ( 'NONE',  ( -1.000000000000000000, 0.000000000000000000, 0.000000000000000000 ) ) ;
#15767=VERTEX_POINT ( 'NONE', #1704 ) ;
#15807=DIRECTION ( 'NONE',  ( 1.000000000000000000, 0.000000000000000000, 0.000000000000000000 ) ) ;
#15825=DIRECTION ( 'NONE',  ( 0.000000000000000000, 0.000000000000000000, -1.000000000000000000 ) ) ;
#15826=PRODUCT_DEFINITION ( 'UNKNOWN', '', #900, #46835 ) ;
#15830=ORIENTED_EDGE ( 'NONE', *, *, #19585, .F. ) ;
#15836=AXIS2_PLACEMENT_3D ( 'NONE', #25432, #44859, #41183 ) ;
#15855=CARTESIAN_POINT ( 'NONE',  ( 16.13393739769620083, -15.61618894467929941, -1.149999999999999911 ) ) ;
#15877=CIRCLE ( 'NONE', #45174, 5.499999999999998224 ) ;
#15896=CARTESIAN_POINT ( 'NONE',  ( 51.13393739769620083, -15.61618894467929941, 9.349999999999999645 ) ) ;
#15910=VECTOR ( 'NONE', #19849, 1000.000000000000000 ) ;
#15913=ORIENTED_EDGE ( 'NONE', *, *, #4554, .T. ) ;
#15976=ORIENTED_EDGE ( 'NONE', *, *, #26461, .F. ) ;
#16065=ADVANCED_FACE ( 'NONE', ( #7651 ), #12341, .T. ) ;
#16084=AXIS2_PLACEMENT_3D ( 'NONE', #12487, #28712, #44456 ) ;
#16088=CARTESIAN_POINT ( 'NONE',  ( -18.86606260230390220, 19.38381105532060289, 11.34999999999999964 ) ) ;
#16098=DIRECTION ( 'NONE',  ( 1.000000000000000000, 0.000000000000000000, 0.000000000000000000 ) ) ;
#16101=DIRECTION ( 'NONE',  ( 0.000000000000000000, 0.000000000000000000, -1.000000000000000000 ) ) ;
#16115=CIRCLE ( 'NONE', #47124, 17.63819660112499932 ) ;
#16134=DIRECTION ( 'NONE',  ( 0.000000000000000000, 1.000000000000000000, 0.000000000000000000 ) ) ;
#16176=CIRCLE ( 'NONE', #45477, 10.00000000000000711 ) ;
#16193=VECTOR ( 'NONE', #11089, 1000.000000000000000 ) ;
#16205=ORIENTED_EDGE ( 'NONE', *, *, #41269, .F. ) ;
#16208=DIRECTION ( 'NONE',  ( 1.000000000000000000, 0.000000000000000000, 0.000000000000000000 ) ) ;
#16228=DIRECTION ( 'NONE',  ( 1.000000000000000000, 1.222653822078627158E-29, -4.718060457820110146E-11 ) ) ;
#16234=DIRECTION ( 'NONE',  ( 0.000000000000000000, 0.000000000000000000, -1.000000000000000000 ) ) ;
#16235=AXIS2_PLACEMENT_3D ( 'NONE', #34821, #30880, #19619 ) ;
#16237=CARTESIAN_POINT ( 'NONE',  ( 53.63393739769619373, -53.11618894467930119, 11.84999999999999964 ) ) ;
#16245=PRODUCT_CONTEXT ( 'NONE', #37159, 'mechanical' ) ;
#16254=EDGE_CURVE ( 'NONE', #49131, #28918, #37793, .T. ) ;
#16262=AXIS2_PLACEMENT_3D ( 'NONE', #23288, #19384, #31414 ) ;
#16294=VERTEX_POINT ( 'NONE', #23023 ) ;
#16308=EDGE_CURVE ( 'NONE', #48268, #32800, #51087, .T. ) ;
#16350=VERTEX_POINT ( 'NONE', #46915 ) ;
#16351=VERTEX_POINT ( 'NONE', #10741 ) ;
#16362=ORIENTED_EDGE ( 'NONE', *, *, #799, .T. ) ;
#16397=VERTEX_POINT ( 'NONE', #19367 ) ;
#16409=ORIENTED_EDGE ( 'NONE', *, *, #44531, .F. ) ;
#16419=CIRCLE ( 'NONE', #6406, 5.499999999999998224 ) ;
#16420=VERTEX_POINT ( 'NONE', #7326 ) ;
#16438=DIRECTION ( 'NONE',  ( 0.000000000000000000, 0.000000000000000000, 1.000000000000000000 ) ) ;
#16441=CYLINDRICAL_SURFACE ( 'NONE', #34052, 6.100000000000001421 ) ;
#16442=CYLINDRICAL_SURFACE ( 'NONE', #26249, 1.000000000000003775 ) ;
#16449=EDGE_CURVE ( 'NONE', #434, #49131, #39448, .T. ) ;
#16457=FACE_BOUND ( 'NONE', #3807, .T. ) ;
#16462=DIRECTION ( 'NONE',  ( 0.000000000000000000, 1.000000000000000000, 0.000000000000000000 ) ) ;
#16470=CARTESIAN_POINT ( 'NONE',  ( -31.36606260230380272, 31.88381105532069881, 17.35000000000000142 ) ) ;
#16473=ORIENTED_EDGE ( 'NONE', *, *, #5162, .F. ) ;
#16488=EDGE_CURVE ( 'NONE', #50414, #7343, #224, .T. ) ;
#16514=DIRECTION ( 'NONE',  ( -9.408764999999898798E-18, 1.274833000000000002E-16, 1.000000000000000000 ) ) ;
#16560=( LENGTH_UNIT ( ) NAMED_UNIT ( * ) SI_UNIT ( .MILLI., .METRE. ) );
#16561=ORIENTED_EDGE ( 'NONE', *, *, #27382, .T. ) ;
#16578=VERTEX_POINT ( 'NONE', #36121 ) ;
#16635=EDGE_LOOP ( 'NONE', ( #21224, #19605, #44252, #28314 ) ) ;
#16654=EDGE_LOOP ( 'NONE', ( #21106, #8343, #42698, #25371 ) ) ;
#16668=VERTEX_POINT ( 'NONE', #25081 ) ;
#16677=VERTEX_POINT ( 'NONE', #21416 ) ;
#16688=CARTESIAN_POINT ( 'NONE',  ( 53.63393739769619373, -53.11618894467930119, 11.84999999999999964 ) ) ;
#16707=LINE ( 'NONE', #25063, #44734 ) ;
#16715=DIRECTION ( 'NONE',  ( 1.000000000000000000, 0.000000000000000000, 0.000000000000000000 ) ) ;
#16720=VECTOR ( 'NONE', #39265, 1000.000000000000000 ) ;
#16723=AXIS2_PLACEMENT_3D ( 'NONE', #27784, #2665, #11307 ) ;
#16755=ORIENTED_EDGE ( 'NONE', *, *, #37633, .F. ) ;
#16756=CARTESIAN_POINT ( 'NONE',  ( 51.13393739769659874, -50.61618894467899565, 16.85000000000000142 ) ) ;
#16801=DIRECTION ( 'NONE',  ( 0.7071067811865457964, 0.000000000000000000, -0.7071067811865492381 ) ) ;
#16805=DIRECTION ( 'NONE',  ( 0.000000000000000000, 0.000000000000000000, -1.000000000000000000 ) ) ;
#16809=CARTESIAN_POINT ( 'NONE',  ( 29.63393739769620083, -15.61618894467929941, 17.35000000000000142 ) ) ;
#16816=ORIENTED_EDGE ( 'NONE', *, *, #51702, .T. ) ;
#16823=DIRECTION ( 'NONE',  ( 0.000000000000000000, 0.000000000000000000, 1.000000000000000000 ) ) ;
#16847=CARTESIAN_POINT ( 'NONE',  ( 53.63393739769619373, -63.11618894467929408, 11.84999999999999964 ) ) ;
#16884=DIRECTION ( 'NONE',  ( -0.000000000000000000, 1.000000000000000000, 0.000000000000000000 ) ) ;
#16914=UNCERTAINTY_MEASURE_WITH_UNIT (LENGTH_MEASURE( 1.000000000000000082E-05 ), #16560, 'distance_accuracy_value', 'NONE');
#16917=EDGE_CURVE ( 'NONE', #16944, #35239, #40333, .T. ) ;
#16932=ORIENTED_EDGE ( 'NONE', *, *, #704, .F. ) ;
#16933=DIRECTION ( 'NONE',  ( 1.000000000000000000, 0.000000000000000000, 0.000000000000000000 ) ) ;
#16944=VERTEX_POINT ( 'NONE', #15896 ) ;
#16970=ADVANCED_FACE ( 'NONE', ( #27930 ), #33627, .F. ) ;
#16971=DIRECTION ( 'NONE',  ( 1.000000000000000000, 0.000000000000000000, 0.000000000000000000 ) ) ;
#16984=PLANE ( 'NONE',  #11263 ) ;
#17007=FACE_OUTER_BOUND ( 'NONE', #18171, .T. ) ;
#17017=DIRECTION ( 'NONE',  ( 1.000000000000000000, 0.000000000000000000, 0.000000000000000000 ) ) ;
#17026=LINE ( 'NONE', #13110, #48614 ) ;
#17039=CYLINDRICAL_SURFACE ( 'NONE', #35955, 6.100000000000001421 ) ;
#17044=FACE_BOUND ( 'NONE', #5627, .T. ) ;
#17054=CARTESIAN_POINT ( 'NONE',  ( 16.13393739769620083, -15.61618894467929941, -18.08174999999999955 ) ) ;
#17087=DIRECTION ( 'NONE',  ( 1.000000000000000000, 0.000000000000000000, 0.000000000000000000 ) ) ;
#17111=CYLINDRICAL_SURFACE ( 'NONE', #25697, 10.00000000000000888 ) ;
#17116=EDGE_LOOP ( 'NONE', ( #36984, #13731, #40657, #33019 ) ) ;
#17123=DIRECTION ( 'NONE',  ( -1.000000000000000000, 0.000000000000000000, 0.000000000000000000 ) ) ;
#17137=EDGE_LOOP ( 'NONE', ( #19561, #44648, #15073, #25556 ) ) ;
#17150=VERTEX_POINT ( 'NONE', #39746 ) ;
#17185=ORIENTED_EDGE ( 'NONE', *, *, #25145, .F. ) ;
#17208=PLANE ( 'NONE',  #25129 ) ;
#17229=AXIS2_PLACEMENT_3D ( 'NONE', #9628, #13814, #17235 ) ;
#17235=DIRECTION ( 'NONE',  ( 0.8090169943749473402, 0.5877852522924732481, 0.000000000000000000 ) ) ;
#17280=FACE_BOUND ( 'NONE', #28761, .T. ) ;
#17288=FACE_OUTER_BOUND ( 'NONE', #27628, .T. ) ;
#17290=ORIENTED_EDGE ( 'NONE', *, *, #50685, .T. ) ;
#17345=ORIENTED_EDGE ( 'NONE', *, *, #33638, .T. ) ;
#17381=EDGE_CURVE ( 'NONE', #25261, #44616, #5443, .T. ) ;
#17393=EDGE_LOOP ( 'NONE', ( #20310, #51234, #11665, #33639 ) ) ;
#17399=DIRECTION ( 'NONE',  ( 0.000000000000000000, 0.000000000000000000, -1.000000000000000000 ) ) ;
#17405=EDGE_LOOP ( 'NONE', ( #16409, #45657, #5668, #16755 ) ) ;
#17408=ADVANCED_FACE ( 'NONE', ( #46054 ), #22168, .F. ) ;
#17424=ORIENTED_EDGE ( 'NONE', *, *, #110, .F. ) ;
#17434=EDGE_CURVE ( 'NONE', #50028, #9032, #50748, .T. ) ;
#17443=ORIENTED_EDGE ( 'NONE', *, *, #7869, .T. ) ;
#17453=CARTESIAN_POINT ( 'NONE',  ( 16.13393739769620083, -15.61618894467929941, -9.721247897589949005 ) ) ;
#17462=ORIENTED_EDGE ( 'NONE', *, *, #44104, .F. ) ;
#17463=VERTEX_POINT ( 'NONE', #398 ) ;
#17489=CARTESIAN_POINT ( 'NONE',  ( -18.86606260230360022, -50.61618894467959962, 16.21999999999999886 ) ) ;
#17501=ORIENTED_EDGE ( 'NONE', *, *, #22992, .F. ) ;
#17511=CARTESIAN_POINT ( 'NONE',  ( 16.13393739846139852, -15.61618894397629909, 14.85000000048049884 ) ) ;
#17525=AXIS2_PLACEMENT_3D ( 'NONE', #42007, #2168, #41477 ) ;
#17552=CIRCLE ( 'NONE', #46867, 1.000000000000000888 ) ;
#17562=AXIS2_PLACEMENT_3D ( 'NONE', #5143, #5396, #16933 ) ;
#17596=CIRCLE ( 'NONE', #34284, 5.999999999999998224 ) ;
#17600=CARTESIAN_POINT ( 'NONE',  ( 16.13393739769620083, -15.61618894467939889, 17.35000000000000142 ) ) ;
#17603=LINE ( 'NONE', #49327, #37041 ) ;
#17605=AXIS2_PLACEMENT_3D ( 'NONE', #44405, #37316, #16101 ) ;
#17622=ORIENTED_EDGE ( 'NONE', *, *, #51861, .F. ) ;
#17648=EDGE_LOOP ( 'NONE', ( #22198, #3992, #40841, #35944 ) ) ;
#17657=VERTEX_POINT ( 'NONE', #9510 ) ;
#17676=DIRECTION ( 'NONE',  ( 7.719205000000000365E-17, 1.062456999999999985E-16, 1.000000000000000000 ) ) ;
#17692=EDGE_CURVE ( 'NONE', #16294, #50249, #20227, .T. ) ;
#17699=CYLINDRICAL_SURFACE ( 'NONE', #17562, 5.499999999999998224 ) ;
#17710=ORIENTED_EDGE ( 'NONE', *, *, #42591, .T. ) ;
#17721=ORIENTED_EDGE ( 'NONE', *, *, #36010, .T. ) ;
#17748=CARTESIAN_POINT ( 'NONE',  ( 24.88393739769619728, -15.61618894467929941, 14.34999999999999964 ) ) ;
#17754=CYLINDRICAL_SURFACE ( 'NONE', #15378, 4.649999999999999467 ) ;
#17763=DIRECTION ( 'NONE',  ( -1.000000000000000000, 0.000000000000000000, 0.000000000000000000 ) ) ;
#17783=VERTEX_POINT ( 'NONE', #24871 ) ;
#17791=ORIENTED_EDGE ( 'NONE', *, *, #21826, .T. ) ;
#17796=DIRECTION ( 'NONE',  ( 0.000000000000000000, 1.000000000000000000, 0.000000000000000000 ) ) ;
#17797=DIRECTION ( 'NONE',  ( -0.8090169943749477843, -0.5877852522924728040, 0.000000000000000000 ) ) ;
#17798=EDGE_CURVE ( 'NONE', #13741, #29295, #7690, .T. ) ;
#17816=ORIENTED_EDGE ( 'NONE', *, *, #31846, .T. ) ;
#17825=CARTESIAN_POINT ( 'NONE',  ( 10.03393739769619941, -15.61618894467929941, -8.849999999999999645 ) ) ;
#17866=CARTESIAN_POINT ( 'NONE',  ( -31.36606260230380272, -62.11618894467930119, 11.84999999999999964 ) ) ;
#17889=CARTESIAN_POINT ( 'NONE',  ( 6.133937397696199945, -15.61618894467930119, -5.966499999999999915 ) ) ;
#17892=DIRECTION ( 'NONE',  ( 0.7071067811865473507, 0.7071067811865476838, 0.000000000000000000 ) ) ;
#17919=CARTESIAN_POINT ( 'NONE',  ( -30.36606260230379917, -53.11618894467940066, 16.35000000000000142 ) ) ;
#17922=AXIS2_PLACEMENT_3D ( 'NONE', #33207, #32941, #48435 ) ;
#17923=ORIENTED_EDGE ( 'NONE', *, *, #27404, .F. ) ;
#17932=EDGE_LOOP ( 'NONE', ( #28192, #7257 ) ) ;
#17934=TOROIDAL_SURFACE ( 'NONE', #47255, 9.000000000000000000, 1.000000000000000000 ) ;
#17963=ORIENTED_EDGE ( 'NONE', *, *, #13192, .F. ) ;
#17966=VERTEX_POINT ( 'NONE', #50330 ) ;
#17976=CARTESIAN_POINT ( 'NONE',  ( 51.13393739769659874, -50.61618894467899565, 16.21999999999999886 ) ) ;
#17992=CARTESIAN_POINT ( 'NONE',  ( -15.63324371469531116, 23.83340452438281076, 11.34999999999999964 ) ) ;
#17993=VERTEX_POINT ( 'NONE', #51803 ) ;
#17996=DIRECTION ( 'NONE',  ( 0.000000000000000000, 0.000000000000000000, -1.000000000000000000 ) ) ;
#18019=FACE_OUTER_BOUND ( 'NONE', #49703, .T. ) ;
#18025=EDGE_CURVE ( 'NONE', #12701, #1900, #6905, .T. ) ;
#18032=ORIENTED_EDGE ( 'NONE', *, *, #17434, .T. ) ;
#18045=CIRCLE ( 'NONE', #43156, 10.00000000000000711 ) ;
#18048=AXIS2_PLACEMENT_3D ( 'NONE', #43352, #47294, #18459 ) ;
#18064=CARTESIAN_POINT ( 'NONE',  ( -18.86606260230390220, 19.38381105532060289, 17.35000000000000142 ) ) ;
#18075=CIRCLE ( 'NONE', #35667, 1.000000000000000888 ) ;
#18109=DIRECTION ( 'NONE',  ( 0.000000000000000000, -1.000000000000000000, 0.000000000000000000 ) ) ;
#18111=EDGE_CURVE ( 'NONE', #8558, #35579, #50411, .T. ) ;
#18141=AXIS2_PLACEMENT_3D ( 'NONE', #21536, #33335, #32799 ) ;
#18148=FACE_BOUND ( 'NONE', #20915, .T. ) ;
#18158=AXIS2_PLACEMENT_3D ( 'NONE', #45820, #5724, #41881 ) ;
#18163=VERTEX_POINT ( 'NONE', #47122 ) ;
#18166=ORIENTED_EDGE ( 'NONE', *, *, #19847, .F. ) ;
#18171=EDGE_LOOP ( 'NONE', ( #26239, #37193, #47380, #29042 ) ) ;
#18203=DIRECTION ( 'NONE',  ( 0.000000000000000000, -1.000000000000000000, 0.000000000000000000 ) ) ;
#18226=VECTOR ( 'NONE', #22666, 1000.000000000000000 ) ;
#18249=EDGE_CURVE ( 'NONE', #44616, #33500, #26093, .T. ) ;
#18261=ORIENTED_EDGE ( 'NONE', *, *, #163, .F. ) ;
#18279=CARTESIAN_POINT ( 'NONE',  ( -7.616062602303800055, -62.11618894467930119, 16.35000000000000142 ) ) ;
#18292=ORIENTED_EDGE ( 'NONE', *, *, #19288, .T. ) ;
#18306=DIRECTION ( 'NONE',  ( 1.000000000000000000, 0.000000000000000000, 0.000000000000000000 ) ) ;
#18307=VERTEX_POINT ( 'NONE', #27884 ) ;
#18309=EDGE_CURVE ( 'NONE', #30599, #48268, #51247, .T. ) ;
#18317=DIRECTION ( 'NONE',  ( 1.000000000000000000, 0.000000000000000000, 0.000000000000000000 ) ) ;
#18321=ORIENTED_EDGE ( 'NONE', *, *, #2141, .T. ) ;
#18337=ORIENTED_EDGE ( 'NONE', *, *, #42944, .T. ) ;
#18355=EDGE_LOOP ( 'NONE', ( #33561, #16816, #22788, #8834 ) ) ;
#18357=CARTESIAN_POINT ( 'NONE',  ( 63.34104417888273986, 21.88381105532059934, 11.14289321881345174 ) ) ;
#18378=EDGE_CURVE ( 'NONE', #27172, #18529, #39516, .T. ) ;
#18387=CARTESIAN_POINT ( 'NONE',  ( 15.26098176771331438, -16.25042833492357985, -14.88746750000000141 ) ) ;
#18389=EDGE_LOOP ( 'NONE', ( #15696, #30471, #32984, #39709, #42998, #30911 ) ) ;
#18405=CIRCLE ( 'NONE', #2512, 18.86180339887500068 ) ;
#18413=CIRCLE ( 'NONE', #41869, 10.00000000000000888 ) ;
#18427=FACE_BOUND ( 'NONE', #9794, .T. ) ;
#18432=DIRECTION ( 'NONE',  ( -1.000000000000000000, 0.000000000000000000, 0.000000000000000000 ) ) ;
#18439=ADVANCED_FACE ( 'NONE', ( #5864 ), #38618, .T. ) ;
#18459=DIRECTION ( 'NONE',  ( -1.000000000000000000, 0.000000000000000000, 0.000000000000000000 ) ) ;
#18473=VERTEX_POINT ( 'NONE', #19456 ) ;
#18483=VERTEX_POINT ( 'NONE', #30727 ) ;
#18490=EDGE_CURVE ( 'NONE', #17993, #8898, #7723, .T. ) ;
#18508=DIRECTION ( 'NONE',  ( 0.000000000000000000, 0.000000000000000000, -1.000000000000000000 ) ) ;
#18510=EDGE_CURVE ( 'NONE', #6855, #42670, #6110, .T. ) ;
#18518=AXIS2_PLACEMENT_3D ( 'NONE', #3654, #8097, #43739 ) ;
#18529=VERTEX_POINT ( 'NONE', #48274 ) ;
#18587=AXIS2_PLACEMENT_3D ( 'NONE', #14243, #13734, #34398 ) ;
#18589=CIRCLE ( 'NONE', #33630, 10.00000000000000711 ) ;
#18591=AXIS2_PLACEMENT_3D ( 'NONE', #8462, #40683, #39660 ) ;
#18595=DIRECTION ( 'NONE',  ( -1.062456999999999985E-16, 7.719205000000000365E-17, 1.000000000000000000 ) ) ;
#18609=CARTESIAN_POINT ( 'NONE',  ( -22.09888148991248968, 14.93421758625839146, 11.34999999999999964 ) ) ;
#18651=DIRECTION ( 'NONE',  ( 0.8090169943749462300, -0.5877852522924749135, 0.000000000000000000 ) ) ;
#18661=CYLINDRICAL_SURFACE ( 'NONE', #22483, 1.000000000000001332 ) ;
#18671=TOROIDAL_SURFACE ( 'NONE', #21977, 19.30901699437490038, 0.5000000000000000000 ) ;
#18676=ORIENTED_EDGE ( 'NONE', *, *, #35058, .T. ) ;
#18680=ORIENTED_EDGE ( 'NONE', *, *, #37362, .T. ) ;
#18692=DIRECTION ( 'NONE',  ( 0.000000000000000000, -1.000000000000000000, 0.000000000000000000 ) ) ;
#18694=DIRECTION ( 'NONE',  ( 1.000000000000000000, 0.000000000000000000, 0.000000000000000000 ) ) ;
#18702=CIRCLE ( 'NONE', #12020, 0.5000000000822003576 ) ;
#18728=DIRECTION ( 'NONE',  ( 0.000000000000000000, 0.000000000000000000, -1.000000000000000000 ) ) ;
#18765=VERTEX_POINT ( 'NONE', #47132 ) ;
#18775=DIRECTION ( 'NONE',  ( 1.000000000000000000, 0.000000000000000000, 0.000000000000000000 ) ) ;
#18779=CIRCLE ( 'NONE', #43896, 1.000000000000000000 ) ;
#18802=EDGE_CURVE ( 'NONE', #26465, #8898, #26133, .T. ) ;
#18812=DIRECTION ( 'NONE',  ( 0.000000000000000000, 0.000000000000000000, -1.000000000000000000 ) ) ;
#18836=DIRECTION ( 'NONE',  ( 0.000000000000000000, 0.000000000000000000, 1.000000000000000000 ) ) ;
#18840=DIRECTION ( 'NONE',  ( -0.4156269377774487461, -0.5720614028176871368, -0.7071067811865479058 ) ) ;
#18843=VERTEX_POINT ( 'NONE', #11992 ) ;
#18853=CARTESIAN_POINT ( 'NONE',  ( 16.13393739769620083, -15.61618894467929941, 17.35000000000000142 ) ) ;
#18868=ORIENTED_EDGE ( 'NONE', *, *, #17692, .F. ) ;
#18869=CONICAL_SURFACE ( 'NONE', #44801, 9.750000000000000000, 0.7853981633974476129 ) ;
#18909=DIRECTION ( 'NONE',  ( 0.000000000000000000, 1.000000000000000000, 0.000000000000000000 ) ) ;
#18934=ADVANCED_FACE ( 'NONE', ( #44466 ), #36589, .T. ) ;
#18940=FACE_OUTER_BOUND ( 'NONE', #8946, .T. ) ;
#18954=CARTESIAN_POINT ( 'NONE',  ( 36.13393739769620083, -15.61618894467929941, -15.18999999999999950 ) ) ;
#18986=CARTESIAN_POINT ( 'NONE',  ( 46.68434392863400717, 22.61662994292931117, 11.34999999999999964 ) ) ;
#18995=AXIS2_PLACEMENT_3D ( 'NONE', #27016, #22556, #43023 ) ;
#19023=EDGE_CURVE ( 'NONE', #32963, #1782, #16115, .T. ) ;
#19030=DIRECTION ( 'NONE',  ( 0.000000000000000000, 0.000000000000000000, 1.000000000000000000 ) ) ;
#19079=CARTESIAN_POINT ( 'NONE',  ( -7.616062602303800055, -62.82329572586585442, 17.05710678118654755 ) ) ;
#19082=DIRECTION ( 'NONE',  ( 1.000000000000000000, 0.000000000000000000, 0.000000000000000000 ) ) ;
#19124=AXIS2_PLACEMENT_3D ( 'NONE', #14885, #9920, #25883 ) ;
#19158=CIRCLE ( 'NONE', #12459, 10.00000000000000355 ) ;
#19173=DIRECTION ( 'NONE',  ( -1.000000000000000000, 0.000000000000000000, 0.000000000000000000 ) ) ;
#19196=AXIS2_PLACEMENT_3D ( 'NONE', #44796, #21185, #48471 ) ;
#19202=AXIS2_PLACEMENT_3D ( 'NONE', #13900, #30823, #3328 ) ;
#19207=DIRECTION ( 'NONE',  ( -0.5720614028176829180, -0.4156269377774549634, 0.7071067811865477948 ) ) ;
#19227=AXIS2_PLACEMENT_3D ( 'NONE', #48144, #8306, #12244 ) ;
#19246=VERTEX_POINT ( 'NONE', #13455 ) ;
#19258=DIRECTION ( 'NONE',  ( 0.000000000000000000, -1.000000000000000000, 0.000000000000000000 ) ) ;
#19288=EDGE_CURVE ( 'NONE', #44094, #30599, #49099, .T. ) ;
#19344=AXIS2_PLACEMENT_3D ( 'NONE', #889, #16884, #16098 ) ;
#19353=DIRECTION ( 'NONE',  ( 0.000000000000000000, 0.000000000000000000, 1.000000000000000000 ) ) ;
#19355=CARTESIAN_POINT ( 'NONE',  ( -21.36606260230379917, -53.11618894467930119, 11.84999999999999964 ) ) ;
#19358=DIRECTION ( 'NONE',  ( 0.000000000000000000, 1.000000000000000000, 0.000000000000000000 ) ) ;
#19361=LINE ( 'NONE', #50825, #48870 ) ;
#19367=CARTESIAN_POINT ( 'NONE',  ( 28.63393739769620083, -15.61618894467929941, -2.149999999999999911 ) ) ;
#19384=DIRECTION ( 'NONE',  ( -1.838191881340036742E-22, -1.000000000000000000, 6.470619327693540153E-12 ) ) ;
#19390=EDGE_CURVE ( 'NONE', #49436, #7343, #11161, .T. ) ;
#19413=FACE_OUTER_BOUND ( 'NONE', #3289, .T. ) ;
#19416=EDGE_CURVE ( 'NONE', #13604, #9988, #22021, .T. ) ;
#19451=ORIENTED_EDGE ( 'NONE', *, *, #20482, .F. ) ;
#19456=CARTESIAN_POINT ( 'NONE',  ( -30.36606260230379917, -53.11618894467930119, 10.84999999999999964 ) ) ;
#19466=CARTESIAN_POINT ( 'NONE',  ( -30.36606260230379917, 21.88381105532059934, 11.84999999999999964 ) ) ;
#19467=DIRECTION ( 'NONE',  ( 0.7071067811865475727, -0.7071067811865475727, 0.000000000000000000 ) ) ;
#19485=VECTOR ( 'NONE', #16462, 1000.000000000000000 ) ;
#19487=VECTOR ( 'NONE', #13983, 1000.000000000000000 ) ;
#19505=DIRECTION ( 'NONE',  ( 0.000000000000000000, 0.000000000000000000, -1.000000000000000000 ) ) ;
#19506=VERTEX_POINT ( 'NONE', #789 ) ;
#19525=AXIS2_PLACEMENT_3D ( 'NONE', #34510, #5974, #46079 ) ;
#19548=DIRECTION ( 'NONE',  ( 0.000000000000000000, 0.000000000000000000, 1.000000000000000000 ) ) ;
#19551=EDGE_CURVE ( 'NONE', #44765, #235, #12848, .T. ) ;
#19561=ORIENTED_EDGE ( 'NONE', *, *, #29835, .F. ) ;
#19579=ORIENTED_EDGE ( 'NONE', *, *, #14794, .T. ) ;
#19585=EDGE_CURVE ( 'NONE', #28389, #42488, #38258, .T. ) ;
#19598=LINE ( 'NONE', #22996, #15910 ) ;
#19605=ORIENTED_EDGE ( 'NONE', *, *, #44531, .T. ) ;
#19619=DIRECTION ( 'NONE',  ( 1.000000000000000000, 0.000000000000000000, 0.000000000000000000 ) ) ;
#19632=CARTESIAN_POINT ( 'NONE',  ( 53.63393739769619373, 30.88381105532059934, 10.84999999999999964 ) ) ;
#19634=AXIS2_PLACEMENT_3D ( 'NONE', #11953, #27908, #23959 ) ;
#19642=CARTESIAN_POINT ( 'NONE',  ( -18.86606260230390220, 24.88381105532059934, 11.34999999999999964 ) ) ;
#19648=EDGE_CURVE ( 'NONE', #29295, #16677, #728, .T. ) ;
#19663=ORIENTED_EDGE ( 'NONE', *, *, #31561, .T. ) ;
#19682=VERTEX_POINT ( 'NONE', #13078 ) ;
#19701=CARTESIAN_POINT ( 'NONE',  ( 29.13393739769620083, -15.61618894467929941, -6.189999999999999503 ) ) ;
#19722=FACE_BOUND ( 'NONE', #50195, .T. ) ;
#19729=AXIS2_PLACEMENT_3D ( 'NONE', #17489, #38181, #37922 ) ;
#19737=DIRECTION ( 'NONE',  ( 0.000000000000000000, 0.000000000000000000, -1.000000000000000000 ) ) ;
#19754=CONICAL_SURFACE ( 'NONE', #14748, 0.6299999999999942313, 0.7853981633974476129 ) ;
#19782=ORIENTED_EDGE ( 'NONE', *, *, #37789, .T. ) ;
#19783=ORIENTED_EDGE ( 'NONE', *, *, #2141, .F. ) ;
#19790=EDGE_CURVE ( 'NONE', #46911, #49915, #4481, .T. ) ;
#19795=VECTOR ( 'NONE', #2413, 1000.000000000000114 ) ;
#19804=ADVANCED_FACE ( 'NONE', ( #46591 ), #17754, .F. ) ;
#19806=CARTESIAN_POINT ( 'NONE',  ( -30.36606260230379917, 21.88381105532059934, 17.35000000000000142 ) ) ;
#19812=DIRECTION ( 'NONE',  ( 1.000000000000000000, 0.000000000000000000, 0.000000000000000000 ) ) ;
#19814=ORIENTED_EDGE ( 'NONE', *, *, #4891, .T. ) ;
#19820=AXIS2_PLACEMENT_3D ( 'NONE', #45594, #6533, #1824 ) ;
#19833=VECTOR ( 'NONE', #37178, 1000.000000000000000 ) ;
#19834=VERTEX_POINT ( 'NONE', #21925 ) ;
#19847=EDGE_CURVE ( 'NONE', #49517, #42477, #1989, .T. ) ;
#19849=DIRECTION ( 'NONE',  ( 0.000000000000000000, 0.000000000000000000, -1.000000000000000000 ) ) ;
#19864=EDGE_CURVE ( 'NONE', #17657, #1082, #12018, .T. ) ;
#19882=ORIENTED_EDGE ( 'NONE', *, *, #20385, .T. ) ;
#19901=PLANE ( 'NONE',  #43382 ) ;
#19917=DIRECTION ( 'NONE',  ( 0.000000000000000000, 0.000000000000000000, -1.000000000000000000 ) ) ;
#19927=EDGE_CURVE ( 'NONE', #14490, #23688, #41301, .T. ) ;
#19932=AXIS2_PLACEMENT_3D ( 'NONE', #15151, #39518, #22988 ) ;
#19964=DIRECTION ( 'NONE',  ( -1.000000000000000000, 0.000000000000000000, 0.000000000000000000 ) ) ;
#19970=AXIS2_PLACEMENT_3D ( 'NONE', #48609, #36796, #4568 ) ;
#19972=CIRCLE ( 'NONE', #49295, 1.000000000000000888 ) ;
#20032=CARTESIAN_POINT ( 'NONE',  ( 16.13393739667419879, -15.61618894434099936, -11.12000000014429979 ) ) ;
#20034=CIRCLE ( 'NONE', #50177, 9.768249999999998323 ) ;
#20035=AXIS2_PLACEMENT_3D ( 'NONE', #10776, #26474, #50085 ) ;
#20036=CIRCLE ( 'NONE', #49374, 5.500000000000000000 ) ;
#20074=ORIENTED_EDGE ( 'NONE', *, *, #22738, .T. ) ;
#20083=TOROIDAL_SURFACE ( 'NONE', #45201, 25.00000000000000000, 3.569999999999939888 ) ;
#20093=EDGE_CURVE ( 'NONE', #19834, #46283, #48825, .T. ) ;
#20129=FACE_OUTER_BOUND ( 'NONE', #43521, .T. ) ;
#20138=ORIENTED_EDGE ( 'NONE', *, *, #14117, .F. ) ;
#20166=DIRECTION ( 'NONE',  ( 0.000000000000000000, 0.000000000000000000, 1.000000000000000000 ) ) ;
#20174=CARTESIAN_POINT ( 'NONE',  ( -18.86606260230390220, 19.38381105532060289, 16.85000000000000142 ) ) ;
#20187=AXIS2_PLACEMENT_3D ( 'NONE', #14565, #33429, #37900 ) ;
#20206=DIRECTION ( 'NONE',  ( 0.7071067811865457964, 0.000000000000000000, 0.7071067811865492381 ) ) ;
#20223=CARTESIAN_POINT ( 'NONE',  ( 51.13393739769620083, -15.61618894467929941, 9.349999999999999645 ) ) ;
#20227=CIRCLE ( 'NONE', #11050, 21.72891455324079857 ) ;
#20240=CARTESIAN_POINT ( 'NONE',  ( -21.36606260230379917, 30.88381105532059934, 16.35000000000000142 ) ) ;
#20241=FACE_OUTER_BOUND ( 'NONE', #10526, .T. ) ;
#20263=DIRECTION ( 'NONE',  ( 0.000000000000000000, 0.000000000000000000, -1.000000000000000000 ) ) ;
#20267=ORIENTED_EDGE ( 'NONE', *, *, #19023, .T. ) ;
#20275=DIRECTION ( 'NONE',  ( 1.000000000000000000, 0.000000000000000000, 0.000000000000000000 ) ) ;
#20280=ORIENTED_EDGE ( 'NONE', *, *, #19927, .F. ) ;
#20284=DIRECTION ( 'NONE',  ( 0.000000000000000000, 0.000000000000000000, 1.000000000000000000 ) ) ;
#20310=ORIENTED_EDGE ( 'NONE', *, *, #18490, .T. ) ;
#20342=EDGE_CURVE ( 'NONE', #24877, #50028, #27078, .T. ) ;
#20343=CARTESIAN_POINT ( 'NONE',  ( -21.36606260230379917, 31.88381105532059934, 16.35000000000000142 ) ) ;
#20373=DIRECTION ( 'NONE',  ( 1.000000000000000000, 0.000000000000000000, 0.000000000000000000 ) ) ;
#20385=EDGE_CURVE ( 'NONE', #39558, #26710, #6186, .T. ) ;
#20387=DIRECTION ( 'NONE',  ( 0.000000000000000000, -1.000000000000000000, 0.000000000000000000 ) ) ;
#20399=ORIENTED_EDGE ( 'NONE', *, *, #50105, .T. ) ;
#20405=DIRECTION ( 'NONE',  ( 0.000000000000000000, 0.000000000000000000, -1.000000000000000000 ) ) ;
#20420=DIRECTION ( 'NONE',  ( 0.000000000000000000, 0.7071067811865457964, -0.7071067811865492381 ) ) ;
#20426=CARTESIAN_POINT ( 'NONE',  ( 16.13393739769620083, -15.61618894467929941, 17.35000000000000142 ) ) ;
#20481=DIRECTION ( 'NONE',  ( -1.000000000000000000, 0.000000000000000000, 0.000000000000000000 ) ) ;
#20482=EDGE_CURVE ( 'NONE', #33390, #42519, #47199, .T. ) ;
#20497=VERTEX_POINT ( 'NONE', #7058 ) ;
#20512=ADVANCED_FACE ( 'NONE', ( #11319 ), #39623, .F. ) ;
#20532=AXIS2_PLACEMENT_3D ( 'NONE', #49021, #8399, #20684 ) ;
#20538=ORIENTED_EDGE ( 'NONE', *, *, #49913, .F. ) ;
#20548=CIRCLE ( 'NONE', #24731, 5.499999999999998224 ) ;
#20618=EDGE_CURVE ( 'NONE', #50796, #30215, #19361, .T. ) ;
#20638=ORIENTED_EDGE ( 'NONE', *, *, #30396, .T. ) ;
#20657=EDGE_CURVE ( 'NONE', #41343, #48021, #44696, .T. ) ;
#20660=CARTESIAN_POINT ( 'NONE',  ( 60.70500520956167634, -60.18725675654477669, 11.84999999999999964 ) ) ;
#20664=DIRECTION ( 'NONE',  ( -0.7071067811865476838, -0.7071067811865473507, 0.000000000000000000 ) ) ;
#20669=CARTESIAN_POINT ( 'NONE',  ( 29.63393739769620083, -15.61618894467929941, -8.655000000000001137 ) ) ;
#20681=EDGE_CURVE ( 'NONE', #38311, #35304, #35510, .T. ) ;
#20684=DIRECTION ( 'NONE',  ( 1.000000000000000000, 0.000000000000000000, 0.000000000000000000 ) ) ;
#20698=CARTESIAN_POINT ( 'NONE',  ( 53.63393739769619373, 30.88381105532059934, 11.84999999999999964 ) ) ;
#20720=EDGE_CURVE ( 'NONE', #26662, #6044, #22917, .T. ) ;
#20724=EDGE_CURVE ( 'NONE', #42519, #30599, #11236, .T. ) ;
#20758=CARTESIAN_POINT ( 'NONE',  ( -21.36606260230379917, -62.11618894467930119, 17.35000000000000142 ) ) ;
#20759=LINE ( 'NONE', #9256, #33199 ) ;
#20765=CARTESIAN_POINT ( 'NONE',  ( 30.40353819813270064, -5.248717105502837654, 14.62639320225000006 ) ) ;
#20782=VERTEX_POINT ( 'NONE', #34754 ) ;
#20789=CARTESIAN_POINT ( 'NONE',  ( -31.07316938349034885, 21.88381105532059934, 11.14289321881345352 ) ) ;
#20799=DIRECTION ( 'NONE',  ( 0.000000000000000000, 0.000000000000000000, 1.000000000000000000 ) ) ;
#20801=DIRECTION ( 'NONE',  ( 0.000000000000000000, 0.000000000000000000, -1.000000000000000000 ) ) ;
#20808=EDGE_CURVE ( 'NONE', #23557, #31144, #36826, .T. ) ;
#20846=VERTEX_POINT ( 'NONE', #159 ) ;
#20876=VECTOR ( 'NONE', #43626, 1000.000000000000114 ) ;
#20894=DIRECTION ( 'NONE',  ( 0.000000000000000000, 0.000000000000000000, 1.000000000000000000 ) ) ;
#20899=AXIS2_PLACEMENT_3D ( 'NONE', #43963, #11496, #46889 ) ;
#20912=ORIENTED_EDGE ( 'NONE', *, *, #8513, .T. ) ;
#20915=EDGE_LOOP ( 'NONE', ( #9136, #23116 ) ) ;
#20918=CARTESIAN_POINT ( 'NONE',  ( 22.23393739769620225, -15.61618894467929941, 2.750000000000000000 ) ) ;
#20922=CARTESIAN_POINT ( 'NONE',  ( 16.13393739954389972, -15.61618894518879941, 4.350000000321379900 ) ) ;
#20940=AXIS2_PLACEMENT_3D ( 'NONE', #26546, #22357, #18694 ) ;
#20946=CARTESIAN_POINT ( 'NONE',  ( 16.13393739769620083, -15.61618894467929941, 14.62639320225000006 ) ) ;
#20947=CIRCLE ( 'NONE', #17605, 1.000000000000000888 ) ;
#20997=ORIENTED_EDGE ( 'NONE', *, *, #33634, .F. ) ;
#21022=ORIENTED_EDGE ( 'NONE', *, *, #10048, .F. ) ;
#21039=CARTESIAN_POINT ( 'NONE',  ( 62.63393739769619373, -53.11618894467930119, 17.35000000000000142 ) ) ;
#21040=DIRECTION ( 'NONE',  ( 0.000000000000000000, 0.000000000000000000, -1.000000000000000000 ) ) ;
#21041=EDGE_CURVE ( 'NONE', #4191, #34457, #50549, .T. ) ;
#21058=CONICAL_SURFACE ( 'NONE', #48687, 0.6299999999999977840, 0.7853981633974476129 ) ;
#21083=AXIS2_PLACEMENT_3D ( 'NONE', #17453, #42076, #6179 ) ;
#21102=CARTESIAN_POINT ( 'NONE',  ( 20.78393739769619941, -15.61618894467929941, -18.35000000000000142 ) ) ;
#21106=ORIENTED_EDGE ( 'NONE', *, *, #18510, .F. ) ;
#21110=EDGE_LOOP ( 'NONE', ( #44794, #1112, #29558, #39056 ) ) ;
#21111=ORIENTED_EDGE ( 'NONE', *, *, #24326, .F. ) ;
#21132=CARTESIAN_POINT ( 'NONE',  ( 52.63393739643800018, -15.61618894418049841, 9.350000000565845681 ) ) ;
#21145=DIRECTION ( 'NONE',  ( 0.000000000000000000, 0.000000000000000000, -1.000000000000000000 ) ) ;
#21151=LINE ( 'NONE', #4660, #25040 ) ;
#21156=AXIS2_PLACEMENT_3D ( 'NONE', #15669, #24010, #7808 ) ;
#21164=CARTESIAN_POINT ( 'NONE',  ( 63.34104417888273986, -53.11618894467930119, 11.14289321881345174 ) ) ;
#21167=DIRECTION ( 'NONE',  ( 0.000000000000000000, 0.000000000000000000, 1.000000000000000000 ) ) ;
#21168=ORIENTED_EDGE ( 'NONE', *, *, #36257, .F. ) ;
#21169=ADVANCED_FACE ( 'NONE', ( #27551 ), #47746, .T. ) ;
#21185=DIRECTION ( 'NONE',  ( 0.000000000000000000, 0.000000000000000000, 1.000000000000000000 ) ) ;
#21213=EDGE_LOOP ( 'NONE', ( #30277, #37414 ) ) ;
#21224=ORIENTED_EDGE ( 'NONE', *, *, #40410, .F. ) ;
#21226=ORIENTED_EDGE ( 'NONE', *, *, #45795, .F. ) ;
#21233=FACE_BOUND ( 'NONE', #27285, .T. ) ;
#21234=DIRECTION ( 'NONE',  ( 0.000000000000000000, 0.000000000000000000, -1.000000000000000000 ) ) ;
#21242=CARTESIAN_POINT ( 'NONE',  ( 53.63393739769619373, -62.11618894467930119, 17.35000000000000142 ) ) ;
#21245=FACE_OUTER_BOUND ( 'NONE', #30589, .T. ) ;
#21246=CARTESIAN_POINT ( 'NONE',  ( -1.866062602303798723, -15.61618894467929763, -18.58999999999999986 ) ) ;
#21280=ADVANCED_FACE ( 'NONE', ( #35933 ), #51, .T. ) ;
#21286=DIRECTION ( 'NONE',  ( 0.000000000000000000, 0.000000000000000000, -1.000000000000000000 ) ) ;
#21364=ORIENTED_EDGE ( 'NONE', *, *, #7034, .T. ) ;
#21365=ORIENTED_EDGE ( 'NONE', *, *, #188, .F. ) ;
#21376=ADVANCED_FACE ( 'NONE', ( #13836 ), #21903, .F. ) ;
#21397=ORIENTED_EDGE ( 'NONE', *, *, #37789, .F. ) ;
#21398=CIRCLE ( 'NONE', #18048, 0.9999999999999974465 ) ;
#21411=ORIENTED_EDGE ( 'NONE', *, *, #12785, .F. ) ;
#21416=CARTESIAN_POINT ( 'NONE',  ( 62.63393739769619373, 21.88381105532059934, 10.84999999999999964 ) ) ;
#21426=ORIENTED_EDGE ( 'NONE', *, *, #31558, .F. ) ;
#21430=DIRECTION ( 'NONE',  ( -1.000000000000000000, 0.000000000000000000, 0.000000000000000000 ) ) ;
#21433=VERTEX_POINT ( 'NONE', #10165 ) ;
#21436=DIRECTION ( 'NONE',  ( 1.000000000000000000, 8.701345253104295327E-30, 2.840828347717470042E-11 ) ) ;
#21444=ORIENTED_EDGE ( 'NONE', *, *, #20720, .T. ) ;
#21466=FACE_OUTER_BOUND ( 'NONE', #47879, .T. ) ;
#21482=CARTESIAN_POINT ( 'NONE',  ( 17.73618694459234391, -14.45208650838193165, -16.68902128623620129 ) ) ;
#21489=ORIENTED_EDGE ( 'NONE', *, *, #24452, .T. ) ;
#21501=ORIENTED_EDGE ( 'NONE', *, *, #4953, .F. ) ;
#21505=FACE_OUTER_BOUND ( 'NONE', #38319, .T. ) ;
#21506=ORIENTED_EDGE ( 'NONE', *, *, #45388, .T. ) ;
#21512=EDGE_LOOP ( 'NONE', ( #48034, #27230, #27309, #886 ) ) ;
#21526=ADVANCED_FACE ( 'NONE', ( #18019 ), #51236, .T. ) ;
#21536=CARTESIAN_POINT ( 'NONE',  ( 35.63393739769620083, -15.61618894467929941, -15.18999999999999950 ) ) ;
#21537=EDGE_LOOP ( 'NONE', ( #43429, #50318, #14236, #8592, #34926, #28591 ) ) ;
#21540=CIRCLE ( 'NONE', #23183, 17.63819660112499932 ) ;
#21541=CARTESIAN_POINT ( 'NONE',  ( -31.36606260230380272, 21.88381105532059934, 11.84999999999999964 ) ) ;
#21555=VERTEX_POINT ( 'NONE', #14091 ) ;
#21574=ORIENTED_EDGE ( 'NONE', *, *, #18249, .T. ) ;
#21577=LINE ( 'NONE', #49393, #48560 ) ;
#21578=ORIENTED_EDGE ( 'NONE', *, *, #51184, .T. ) ;
#21608=DIRECTION ( 'NONE',  ( 0.000000000000000000, 1.000000000000000000, 0.000000000000000000 ) ) ;
#21611=DIRECTION ( 'NONE',  ( -2.490868089198564786E-23, -1.000000000000000000, 1.205421602240320019E-11 ) ) ;
#21616=ORIENTED_EDGE ( 'NONE', *, *, #19790, .F. ) ;
#21644=DIRECTION ( 'NONE',  ( -0.7071067811865475727, -0.7071067811865475727, 0.000000000000000000 ) ) ;
#21651=FACE_OUTER_BOUND ( 'NONE', #31795, .T. ) ;
#21652=CYLINDRICAL_SURFACE ( 'NONE', #13413, 0.9999999999999988898 ) ;
#21658=PLANE ( 'NONE',  #15042 ) ;
#21673=DIRECTION ( 'NONE',  ( 0.000000000000000000, 0.000000000000000000, -1.000000000000000000 ) ) ;
#21680=VECTOR ( 'NONE', #18109, 1000.000000000000000 ) ;
#21683=AXIS2_PLACEMENT_3D ( 'NONE', #10072, #14517, #5635 ) ;
#21710=DIRECTION ( 'NONE',  ( 0.000000000000000000, 0.000000000000000000, 1.000000000000000000 ) ) ;
#21718=AXIS2_PLACEMENT_3D ( 'NONE', #15493, #3184, #31187 ) ;
#21791=EDGE_CURVE ( 'NONE', #48268, #33105, #18589, .T. ) ;
#21798=CIRCLE ( 'NONE', #5880, 17.06999999999999673 ) ;
#21826=EDGE_CURVE ( 'NONE', #13022, #46863, #32107, .T. ) ;
#21832=DIRECTION ( 'NONE',  ( 1.000000000000000000, 0.000000000000000000, 0.000000000000000000 ) ) ;
#21873=CIRCLE ( 'NONE', #51200, 1.000000000000000888 ) ;
#21903=TOROIDAL_SURFACE ( 'NONE', #22765, 36.50000000076989437, 1.500000000038270054 ) ;
#21905=CARTESIAN_POINT ( 'NONE',  ( 51.13393739769659874, -50.61618894467899565, 17.35000000000000142 ) ) ;
#21913=CYLINDRICAL_SURFACE ( 'NONE', #41466, 1.000000000000001332 ) ;
#21925=CARTESIAN_POINT ( 'NONE',  ( -3.866062602303800499, -15.61618894467929763, -15.18999999999999950 ) ) ;
#21929=LINE ( 'NONE', #33981, #14767 ) ;
#21940=CYLINDRICAL_SURFACE ( 'NONE', #15128, 1.000000000000003775 ) ;
#21943=ORIENTED_EDGE ( 'NONE', *, *, #17692, .T. ) ;
#21970=CARTESIAN_POINT ( 'NONE',  ( -21.36606260230379917, -62.11618894467930119, 16.35000000000000142 ) ) ;
#21972=ORIENTED_EDGE ( 'NONE', *, *, #7344, .T. ) ;
#21977=AXIS2_PLACEMENT_3D ( 'NONE', #34732, #42885, #46825 ) ;
#22003=EDGE_CURVE ( 'NONE', #44239, #32442, #26095, .T. ) ;
#22016=ORIENTED_EDGE ( 'NONE', *, *, #17381, .T. ) ;
#22021=CIRCLE ( 'NONE', #42090, 5.999999999999998224 ) ;
#22023=CONICAL_SURFACE ( 'NONE', #51335, 9.750000000000000000, 0.7853981633974476129 ) ;
#22027=EDGE_CURVE ( 'NONE', #12957, #50005, #34455, .T. ) ;
#22050=AXIS2_PLACEMENT_3D ( 'NONE', #51023, #15124, #31082 ) ;
#22053=TOROIDAL_SURFACE ( 'NONE', #39658, 9.000000000000000000, 1.000000000000000000 ) ;
#22062=DIRECTION ( 'NONE',  ( 0.000000000000000000, 0.000000000000000000, -1.000000000000000000 ) ) ;
#22085=DIRECTION ( 'NONE',  ( 0.000000000000000000, 0.000000000000000000, 1.000000000000000000 ) ) ;
#22086=ORIENTED_EDGE ( 'NONE', *, *, #20808, .T. ) ;
#22087=DIRECTION ( 'NONE',  ( 0.000000000000000000, 0.000000000000000000, -1.000000000000000000 ) ) ;
#22146=CIRCLE ( 'NONE', #40562, 6.000000000000000000 ) ;
#22150=EDGE_LOOP ( 'NONE', ( #21943, #40327 ) ) ;
#22167=FILL_AREA_STYLE_COLOUR ( '', #31319 ) ;
#22168=CYLINDRICAL_SURFACE ( 'NONE', #44481, 4.649999999999999467 ) ;
#22182=EDGE_LOOP ( 'NONE', ( #40236, #20638, #26601, #18292 ) ) ;
#22184=CARTESIAN_POINT ( 'NONE',  ( 16.13393739769620083, -15.61618894467929941, 17.07360679774999923 ) ) ;
#22195=DIRECTION ( 'NONE',  ( 0.000000000000000000, -1.000000000000000000, 0.000000000000000000 ) ) ;
#22198=ORIENTED_EDGE ( 'NONE', *, *, #13641, .F. ) ;
#22207=EDGE_CURVE ( 'NONE', #24877, #29876, #17603, .T. ) ;
#22286=DIRECTION ( 'NONE',  ( 0.000000000000000000, 0.000000000000000000, -1.000000000000000000 ) ) ;
#22297=CARTESIAN_POINT ( 'NONE',  ( -21.36606260230379917, -62.11618894467930119, 10.84999999999999964 ) ) ;
#22311=ORIENTED_EDGE ( 'NONE', *, *, #4259, .F. ) ;
#22325=EDGE_CURVE ( 'NONE', #50249, #40580, #14449, .T. ) ;
#22338=ORIENTED_EDGE ( 'NONE', *, *, #16254, .F. ) ;
#22357=DIRECTION ( 'NONE',  ( 0.000000000000000000, 0.000000000000000000, 1.000000000000000000 ) ) ;
#22408=VERTEX_POINT ( 'NONE', #43768 ) ;
#22454=ORIENTED_EDGE ( 'NONE', *, *, #5051, .F. ) ;
#22455=ORIENTED_EDGE ( 'NONE', *, *, #34110, .F. ) ;
#22477=CIRCLE ( 'NONE', #9924, 5.499999999999998224 ) ;
#22483=AXIS2_PLACEMENT_3D ( 'NONE', #45677, #2418, #9779 ) ;
#22500=CARTESIAN_POINT ( 'NONE',  ( 53.63393739769619373, -62.82329572586585442, 11.14289321881345529 ) ) ;
#22506=AXIS2_PLACEMENT_3D ( 'NONE', #44984, #14761, #6643 ) ;
#22520=DIRECTION ( 'NONE',  ( 0.000000000000000000, 0.000000000000000000, 1.000000000000000000 ) ) ;
#22535=DIRECTION ( 'NONE',  ( 0.000000000000000000, 0.000000000000000000, -1.000000000000000000 ) ) ;
#22543=FACE_BOUND ( 'NONE', #31803, .T. ) ;
#22546=DIRECTION ( 'NONE',  ( -0.7071067811865475727, 0.000000000000000000, -0.7071067811865475727 ) ) ;
#22556=DIRECTION ( 'NONE',  ( 0.000000000000000000, 0.000000000000000000, 1.000000000000000000 ) ) ;
#22582=DIRECTION ( 'NONE',  ( 0.000000000000000000, 0.000000000000000000, -1.000000000000000000 ) ) ;
#22586=AXIS2_PLACEMENT_3D ( 'NONE', #31119, #47648, #27710 ) ;
#22595=EDGE_LOOP ( 'NONE', ( #3890, #26916, #9239, #33742 ) ) ;
#22596=ORIENTED_EDGE ( 'NONE', *, *, #12964, .F. ) ;
#22614=VECTOR ( 'NONE', #25321, 1000.000000000000000 ) ;
#22627=VECTOR ( 'NONE', #40667, 1000.000000000000000 ) ;
#22641=FACE_OUTER_BOUND ( 'NONE', #47944, .T. ) ;
#22650=ORIENTED_EDGE ( 'NONE', *, *, #9804, .T. ) ;
#22664=ORIENTED_EDGE ( 'NONE', *, *, #26228, .F. ) ;
#22666=DIRECTION ( 'NONE',  ( 0.000000000000000000, 0.000000000000000000, -1.000000000000000000 ) ) ;
#22679=DIRECTION ( 'NONE',  ( 0.000000000000000000, 0.000000000000000000, 1.000000000000000000 ) ) ;
#22687=DIRECTION ( 'NONE',  ( 0.5720614028176826960, 0.4156269377774550189, 0.7071067811865479058 ) ) ;
#22704=EDGE_LOOP ( 'NONE', ( #33175, #7710, #21397, #22086 ) ) ;
#22712=DIRECTION ( 'NONE',  ( 1.000000000000000000, 0.000000000000000000, 0.000000000000000000 ) ) ;
#22714=CARTESIAN_POINT ( 'NONE',  ( 53.63393739769619373, 31.88381105532059934, 16.35000000000000142 ) ) ;
#22738=EDGE_CURVE ( 'NONE', #16397, #47254, #11125, .T. ) ;
#22759=EDGE_CURVE ( 'NONE', #21433, #17657, #26136, .T. ) ;
#22765=AXIS2_PLACEMENT_3D ( 'NONE', #28837, #14609, #42397 ) ;
#22770=CARTESIAN_POINT ( 'NONE',  ( 53.63393739769619373, 21.88381105532059934, 17.35000000000000142 ) ) ;
#22788=ORIENTED_EDGE ( 'NONE', *, *, #8515, .F. ) ;
#22790=DIRECTION ( 'NONE',  ( -1.000000000000000000, 0.000000000000000000, 0.000000000000000000 ) ) ;
#22862=ORIENTED_EDGE ( 'NONE', *, *, #35422, .F. ) ;
#22913=EDGE_LOOP ( 'NONE', ( #12819, #6006, #41877, #11023, #34726 ) ) ;
#22917=CIRCLE ( 'NONE', #17922, 0.5000000000822003576 ) ;
#22972=ORIENTED_EDGE ( 'NONE', *, *, #26228, .T. ) ;
#22988=DIRECTION ( 'NONE',  ( 1.000000000000000000, -1.703274131079987031E-27, 2.066387465239710029E-12 ) ) ;
#22992=EDGE_CURVE ( 'NONE', #8898, #17993, #33723, .T. ) ;
#22996=CARTESIAN_POINT ( 'NONE',  ( 56.63393739769620083, 19.38381105532069881, 14.21249999999999858 ) ) ;
#23011=LINE ( 'NONE', #26429, #23891 ) ;
#23023=CARTESIAN_POINT ( 'NONE',  ( -5.594977155544602176, -15.61618894467930119, 9.349999999999999645 ) ) ;
#23061=DIRECTION ( 'NONE',  ( 0.000000000000000000, 0.000000000000000000, 1.000000000000000000 ) ) ;
#23063=VERTEX_POINT ( 'NONE', #31623 ) ;
#23075=CONICAL_SURFACE ( 'NONE', #13097, 0.6300000000000018918, 0.7853981633974476129 ) ;
#23116=ORIENTED_EDGE ( 'NONE', *, *, #33638, .F. ) ;
#23119=VECTOR ( 'NONE', #29604, 1000.000000000000000 ) ;
#23130=FACE_OUTER_BOUND ( 'NONE', #31346, .T. ) ;
#23133=DIRECTION ( 'NONE',  ( 0.000000000000000000, 0.000000000000000000, -1.000000000000000000 ) ) ;
#23136=CARTESIAN_POINT ( 'NONE',  ( 36.13393739769620083, -15.61618894467929941, -16.88999999999999702 ) ) ;
#23168=TOROIDAL_SURFACE ( 'NONE', #2273, 9.000000000000000000, 1.000000000000000000 ) ;
#23169=EDGE_LOOP ( 'NONE', ( #50153, #45647, #26741, #34395, #44925 ) ) ;
#23183=AXIS2_PLACEMENT_3D ( 'NONE', #44558, #36678, #36420 ) ;
#23198=CARTESIAN_POINT ( 'NONE',  ( -21.36606260230379917, 21.88381105532059934, 16.35000000000000142 ) ) ;
#23230=ORIENTED_EDGE ( 'NONE', *, *, #29623, .T. ) ;
#23248=LINE ( 'NONE', #19079, #16720 ) ;
#23268=ORIENTED_EDGE ( 'NONE', *, *, #18111, .F. ) ;
#23288=CARTESIAN_POINT ( 'NONE',  ( 33.20393739695829538, -15.61618894434099936, -11.11999999965936858 ) ) ;
#23292=ORIENTED_EDGE ( 'NONE', *, *, #30428, .T. ) ;
#23296=ORIENTED_EDGE ( 'NONE', *, *, #30553, .T. ) ;
#23303=DIRECTION ( 'NONE',  ( 0.8090169943749472292, -0.5877852522924734702, 0.000000000000000000 ) ) ;
#23306=DIRECTION ( 'NONE',  ( -0.7071067811865475727, -0.7071067811865475727, 0.000000000000000000 ) ) ;
#23309=ORIENTED_EDGE ( 'NONE', *, *, #21826, .F. ) ;
#23314=CARTESIAN_POINT ( 'NONE',  ( -21.36606260230379917, 21.88381105532059934, 16.35000000000000142 ) ) ;
#23317=CARTESIAN_POINT ( 'NONE',  ( 51.13393739769659874, -45.11618894467899565, 16.85000000000000142 ) ) ;
#23321=CIRCLE ( 'NONE', #13343, 9.000000000000007105 ) ;
#23329=AXIS2_PLACEMENT_3D ( 'NONE', #11588, #47239, #15765 ) ;
#23338=DIRECTION ( 'NONE',  ( 0.000000000000000000, 0.000000000000000000, 1.000000000000000000 ) ) ;
#23387=CARTESIAN_POINT ( 'NONE',  ( 14.53168785080005776, -16.78029138097666717, -16.68902128623620129 ) ) ;
#23395=CIRCLE ( 'NONE', #16723, 1.500000000038269388 ) ;
#23432=DIRECTION ( 'NONE',  ( -1.000000000000000000, 0.000000000000000000, 0.000000000000000000 ) ) ;
#23447=ORIENTED_EDGE ( 'NONE', *, *, #35422, .T. ) ;
#23456=DIRECTION ( 'NONE',  ( 1.000000000000000000, 0.000000000000000000, 0.000000000000000000 ) ) ;
#23468=LINE ( 'NONE', #39491, #6683 ) ;
#23480=DIRECTION ( 'NONE',  ( 0.000000000000000000, 0.000000000000000000, -1.000000000000000000 ) ) ;
#23529=ORIENTED_EDGE ( 'NONE', *, *, #20657, .T. ) ;
#23540=ORIENTED_EDGE ( 'NONE', *, *, #30788, .T. ) ;
#23542=ORIENTED_EDGE ( 'NONE', *, *, #35198, .F. ) ;
#23557=VERTEX_POINT ( 'NONE', #5943 ) ;
#23560=CARTESIAN_POINT ( 'NONE',  ( 16.13393739769620083, -15.61618894467929941, -15.18999999999999950 ) ) ;
#23679=EDGE_CURVE ( 'NONE', #35239, #16944, #6116, .T. ) ;
#23688=VERTEX_POINT ( 'NONE', #2787 ) ;
#23694=AXIS2_PLACEMENT_3D ( 'NONE', #51405, #43544, #36 ) ;
#23699=ADVANCED_FACE ( 'NONE', ( #34208 ), #18671, .T. ) ;
#23705=LINE ( 'NONE', #31571, #2087 ) ;
#23746=DIRECTION ( 'NONE',  ( -1.000000000000000000, 0.000000000000000000, 0.000000000000000000 ) ) ;
#23777=DIRECTION ( 'NONE',  ( -0.5877852522924661427, -0.8090169943749525583, 0.000000000000000000 ) ) ;
#23787=ORIENTED_EDGE ( 'NONE', *, *, #6820, .F. ) ;
#23807=EDGE_LOOP ( 'NONE', ( #34329, #39710, #38959, #26333, #47054, #37110, #8186, #7481 ) ) ;
#23818=CARTESIAN_POINT ( 'NONE',  ( -21.36606260230379917, 30.88381105532059934, 17.35000000000000142 ) ) ;
#23828=FACE_OUTER_BOUND ( 'NONE', #5874, .T. ) ;
#23854=VECTOR ( 'NONE', #17796, 1000.000000000000000 ) ;
#23858=EDGE_CURVE ( 'NONE', #44239, #3175, #29433, .T. ) ;
#23884=( NAMED_UNIT ( * ) SI_UNIT ( $, .STERADIAN. ) SOLID_ANGLE_UNIT ( ) );
#23891=VECTOR ( 'NONE', #30361, 1000.000000000000000 ) ;
#23906=AXIS2_PLACEMENT_3D ( 'NONE', #6238, #50267, #51294 ) ;
#23959=DIRECTION ( 'NONE',  ( 0.7071067811865457964, 0.000000000000000000, 0.7071067811865492381 ) ) ;
#23972=ORIENTED_EDGE ( 'NONE', *, *, #14607, .F. ) ;
#23985=EDGE_CURVE ( 'NONE', #51387, #44765, #43060, .T. ) ;
#24010=DIRECTION ( 'NONE',  ( 0.000000000000000000, 0.000000000000000000, 1.000000000000000000 ) ) ;
#24034=CARTESIAN_POINT ( 'NONE',  ( 16.13393739769620083, -15.61618894467929941, -18.08174999999999955 ) ) ;
#24040=DIRECTION ( 'NONE',  ( 0.4156269377774524099, 0.5720614028176843613, -0.7071067811865481278 ) ) ;
#24064=ORIENTED_EDGE ( 'NONE', *, *, #41356, .T. ) ;
#24068=FACE_OUTER_BOUND ( 'NONE', #46027, .T. ) ;
#24069=ORIENTED_EDGE ( 'NONE', *, *, #42369, .F. ) ;
#24079=ORIENTED_EDGE ( 'NONE', *, *, #45414, .T. ) ;
#24086=CYLINDRICAL_SURFACE ( 'NONE', #49854, 13.50000000000000178 ) ;
#24137=EDGE_LOOP ( 'NONE', ( #22972, #767 ) ) ;
#24174=AXIS2_PLACEMENT_3D ( 'NONE', #43766, #3943, #7871 ) ;
#24181=AXIS2_PLACEMENT_3D ( 'NONE', #20032, #35781, #11431 ) ;
#24191=EDGE_CURVE ( 'NONE', #16668, #32963, #18702, .T. ) ;
#24194=EDGE_LOOP ( 'NONE', ( #38146, #49390, #18680, #8092 ) ) ;
#24196=DIRECTION ( 'NONE',  ( -1.000000000000000000, 0.000000000000000000, 0.000000000000000000 ) ) ;
#24197=VERTEX_POINT ( 'NONE', #24384 ) ;
#24204=CIRCLE ( 'NONE', #9176, 5.999999999999998224 ) ;
#24223=DIRECTION ( 'NONE',  ( 0.000000000000000000, 0.000000000000000000, -1.000000000000000000 ) ) ;
#24250=ORIENTED_EDGE ( 'NONE', *, *, #36357, .T. ) ;
#24260=LINE ( 'NONE', #4626, #45355 ) ;
#24265=DIRECTION ( 'NONE',  ( 1.000000000000000000, 0.000000000000000000, 0.000000000000000000 ) ) ;
#24273=CIRCLE ( 'NONE', #1711, 10.00000000000000355 ) ;
#24278=DIRECTION ( 'NONE',  ( 0.000000000000000000, 0.000000000000000000, 1.000000000000000000 ) ) ;
#24302=CARTESIAN_POINT ( 'NONE',  ( 16.13393739769620083, -15.61618894467929941, -5.690000000000000391 ) ) ;
#24308=DIRECTION ( 'NONE',  ( 0.000000000000000000, 0.000000000000000000, 1.000000000000000000 ) ) ;
#24318=ORIENTED_EDGE ( 'NONE', *, *, #4953, .T. ) ;
#24326=EDGE_CURVE ( 'NONE', #42283, #25361, #25384, .T. ) ;
#24337=DIRECTION ( 'NONE',  ( 0.000000000000000000, -1.000000000000000000, 0.000000000000000000 ) ) ;
#24339=ORIENTED_EDGE ( 'NONE', *, *, #40321, .F. ) ;
#24343=ADVANCED_FACE ( 'NONE', ( #5729 ), #11195, .F. ) ;
#24347=DIRECTION ( 'NONE',  ( 0.000000000000000000, -1.000000000000000000, 0.000000000000000000 ) ) ;
#24353=DIRECTION ( 'NONE',  ( 0.5877852522924733591, -0.8090169943749473402, 0.000000000000000000 ) ) ;
#24371=ORIENTED_EDGE ( 'NONE', *, *, #7034, .F. ) ;
#24382=ORIENTED_EDGE ( 'NONE', *, *, #34787, .F. ) ;
#24384=CARTESIAN_POINT ( 'NONE',  ( 3.633937397696199056, -15.61618894467929763, -2.149999999999999911 ) ) ;
#24393=CARTESIAN_POINT ( 'NONE',  ( 55.58353086675839450, 16.15099216771209001, 11.34999999999999964 ) ) ;
#24397=DIRECTION ( 'NONE',  ( 0.000000000000000000, -1.000000000000000000, 0.000000000000000000 ) ) ;
#24412=EDGE_LOOP ( 'NONE', ( #14245, #20997 ) ) ;
#24417=DIRECTION ( 'NONE',  ( -0.4156269377774580720, 0.5720614028176802535, 0.7071067811865481278 ) ) ;
#24447=ORIENTED_EDGE ( 'NONE', *, *, #452, .T. ) ;
#24452=EDGE_CURVE ( 'NONE', #18483, #21555, #9518, .T. ) ;
#24455=EDGE_CURVE ( 'NONE', #12281, #29876, #47201, .T. ) ;
#24458=VERTEX_POINT ( 'NONE', #20660 ) ;
#24518=CARTESIAN_POINT ( 'NONE',  ( -21.36606260230379917, 30.88381105532059934, 11.84999999999999964 ) ) ;
#24521=DIRECTION ( 'NONE',  ( 0.000000000000000000, 0.000000000000000000, -1.000000000000000000 ) ) ;
#24543=AXIS2_PLACEMENT_3D ( 'NONE', #45565, #29560, #21436 ) ;
#24571=LINE ( 'NONE', #20918, #19833 ) ;
#24572=ADVANCED_FACE ( 'NONE', ( #38216 ), #22023, .T. ) ;
#24586=CARTESIAN_POINT ( 'NONE',  ( -28.43713041416927823, -60.18725675654476959, 11.84999999999999964 ) ) ;
#24601=CIRCLE ( 'NONE', #7062, 10.49999999999999822 ) ;
#24630=VERTEX_POINT ( 'NONE', #48398 ) ;
#24646=AXIS2_PLACEMENT_3D ( 'NONE', #26345, #50733, #6977 ) ;
#24656=CARTESIAN_POINT ( 'NONE',  ( 24.03661765299927922, -21.35782223538524960, -18.08174999999999955 ) ) ;
#24678=DIRECTION ( 'NONE',  ( 0.000000000000000000, 0.000000000000000000, -1.000000000000000000 ) ) ;
#24708=LINE ( 'NONE', #11930, #31044 ) ;
#24721=DIRECTION ( 'NONE',  ( 1.000000000000000000, 0.000000000000000000, 0.000000000000000000 ) ) ;
#24731=AXIS2_PLACEMENT_3D ( 'NONE', #40325, #21167, #20387 ) ;
#24765=ORIENTED_EDGE ( 'NONE', *, *, #18111, .T. ) ;
#24784=ORIENTED_EDGE ( 'NONE', *, *, #37343, .T. ) ;
#24795=DIRECTION ( 'NONE',  ( -1.000000000000000000, 0.000000000000000000, 0.000000000000000000 ) ) ;
#24831=PLANE ( 'NONE',  #37303 ) ;
#24840=ORIENTED_EDGE ( 'NONE', *, *, #42206, .T. ) ;
#24848=ORIENTED_EDGE ( 'NONE', *, *, #7702, .F. ) ;
#24871=CARTESIAN_POINT ( 'NONE',  ( 60.70500520956167634, -60.18725675654477669, 16.35000000000000142 ) ) ;
#24877=VERTEX_POINT ( 'NONE', #39268 ) ;
#24901=EDGE_LOOP ( 'NONE', ( #25562, #12231 ) ) ;
#24907=CARTESIAN_POINT ( 'NONE',  ( -19.23636731124815569, 18.87413034886438368, 16.21999999999999886 ) ) ;
#24915=ADVANCED_FACE ( 'NONE', ( #26417 ), #22053, .T. ) ;
#24929=CIRCLE ( 'NONE', #19124, 5.500000000000000000 ) ;
#24952=PLANE ( 'NONE',  #28564 ) ;
#24955=DIRECTION ( 'NONE',  ( -3.907280855591541680E-22, -1.000000000000000000, -8.281540456132319756E-12 ) ) ;
#24970=AXIS2_PLACEMENT_3D ( 'NONE', #43081, #26812, #42825 ) ;
#24974=EDGE_LOOP ( 'NONE', ( #36776, #1099, #27820, #41886, #1029 ) ) ;
#24979=CARTESIAN_POINT ( 'NONE',  ( 5.633937397696199056, -15.61618894439688532, -18.58999999999999986 ) ) ;
#24980=ADVANCED_FACE ( 'NONE', ( #48157 ), #16442, .T. ) ;
#25012=ORIENTED_EDGE ( 'NONE', *, *, #32872, .T. ) ;
#25021=ORIENTED_EDGE ( 'NONE', *, *, #44385, .T. ) ;
#25024=ORIENTED_EDGE ( 'NONE', *, *, #51438, .F. ) ;
#25040=VECTOR ( 'NONE', #40825, 1000.000000000000000 ) ;
#25047=AXIS2_PLACEMENT_3D ( 'NONE', #2226, #18203, #50187 ) ;
#25052=FACE_OUTER_BOUND ( 'NONE', #35470, .T. ) ;
#25063=CARTESIAN_POINT ( 'NONE',  ( -3.866062602303800499, -15.61618894467929763, -16.88999999999999702 ) ) ;
#25066=DIRECTION ( 'NONE',  ( -1.000000000000000000, 0.000000000000000000, 0.000000000000000000 ) ) ;
#25076=AXIS2_PLACEMENT_3D ( 'NONE', #3875, #27190, #18812 ) ;
#25080=CARTESIAN_POINT ( 'NONE',  ( 62.63393739769619373, -53.11618894467930119, 10.84999999999999964 ) ) ;
#25081=CARTESIAN_POINT ( 'NONE',  ( -1.057045607928901232, -15.61618894398127999, 14.34999999999999964 ) ) ;
#25123=CIRCLE ( 'NONE', #8390, 10.27649999999999864 ) ;
#25129=AXIS2_PLACEMENT_3D ( 'NONE', #2443, #22087, #6389 ) ;
#25130=DIRECTION ( 'NONE',  ( -1.000000000000000000, 0.000000000000000000, 0.000000000000000000 ) ) ;
#25145=EDGE_CURVE ( 'NONE', #21555, #18765, #28752, .T. ) ;
#25165=LINE ( 'NONE', #16809, #27498 ) ;
#25183=CARTESIAN_POINT ( 'NONE',  ( 51.13393739769659874, -50.61618894467899565, 16.85000000000000142 ) ) ;
#25187=CARTESIAN_POINT ( 'NONE',  ( 26.13393739769619728, -15.61618894467929941, -2.149999999999999911 ) ) ;
#25203=DIRECTION ( 'NONE',  ( -0.7071067811865475727, 0.7071067811865475727, 0.000000000000000000 ) ) ;
#25206=EDGE_LOOP ( 'NONE', ( #22596, #18337, #50276, #23230, #9192 ) ) ;
#25246=EDGE_CURVE ( 'NONE', #18765, #11901, #38634, .T. ) ;
#25261=VERTEX_POINT ( 'NONE', #34976 ) ;
#25265=FACE_OUTER_BOUND ( 'NONE', #28058, .T. ) ;
#25299=EDGE_CURVE ( 'NONE', #9595, #42519, #24708, .T. ) ;
#25307=VERTEX_POINT ( 'NONE', #12962 ) ;
#25315=DIRECTION ( 'NONE',  ( -1.010747651509595448E-22, -1.000000000000000000, 3.858400438143729530E-12 ) ) ;
#25321=DIRECTION ( 'NONE',  ( 0.000000000000000000, 0.000000000000000000, -1.000000000000000000 ) ) ;
#25328=FACE_BOUND ( 'NONE', #24901, .T. ) ;
#25361=VERTEX_POINT ( 'NONE', #36263 ) ;
#25371=ORIENTED_EDGE ( 'NONE', *, *, #5199, .F. ) ;
#25374=VERTEX_POINT ( 'NONE', #20789 ) ;
#25384=CIRCLE ( 'NONE', #41303, 6.000000000000000000 ) ;
#25391=CARTESIAN_POINT ( 'NONE',  ( 63.63393739769619373, 21.88381105532059934, 16.35000000000000142 ) ) ;
#25393=AXIS2_PLACEMENT_3D ( 'NONE', #23560, #11806, #7351 ) ;
#25406=LINE ( 'NONE', #21482, #23119 ) ;
#25424=ADVANCED_FACE ( 'NONE', ( #44399 ), #36781, .T. ) ;
#25432=CARTESIAN_POINT ( 'NONE',  ( 53.63393739769619373, 21.88381105532059934, 11.84999999999999964 ) ) ;
#25449=AXIS2_PLACEMENT_3D ( 'NONE', #33868, #9787, #13213 ) ;
#25451=AXIS2_PLACEMENT_3D ( 'NONE', #32233, #40386, #40130 ) ;
#25461=CARTESIAN_POINT ( 'NONE',  ( -23.31565607136582230, -53.84900783228816579, 16.85000000000000142 ) ) ;
#25476=AXIS2_PLACEMENT_3D ( 'NONE', #8191, #48539, #19964 ) ;
#25480=DIRECTION ( 'NONE',  ( 1.000000000000000000, 0.000000000000000000, 0.000000000000000000 ) ) ;
#25504=DIRECTION ( 'NONE',  ( 0.000000000000000000, 0.000000000000000000, -1.000000000000000000 ) ) ;
#25514=CARTESIAN_POINT ( 'NONE',  ( -18.86606260230390220, 24.88381105532059934, 16.85000000000000142 ) ) ;
#25521=CIRCLE ( 'NONE', #30538, 18.50000000000000000 ) ;
#25548=AXIS2_PLACEMENT_3D ( 'NONE', #31439, #28284, #47468 ) ;
#25550=EDGE_LOOP ( 'NONE', ( #49505, #39383, #18321, #36524 ) ) ;
#25556=ORIENTED_EDGE ( 'NONE', *, *, #41356, .F. ) ;
#25558=CIRCLE ( 'NONE', #32243, 5.999999999999998224 ) ;
#25562=ORIENTED_EDGE ( 'NONE', *, *, #19927, .T. ) ;
#25568=ADVANCED_FACE ( 'NONE', ( #21245 ), #29878, .T. ) ;
#25579=ORIENTED_EDGE ( 'NONE', *, *, #36468, .F. ) ;
#25583=CARTESIAN_POINT ( 'NONE',  ( -19.37574330875981232, -50.24588423573533902, 16.21999999999999886 ) ) ;
#25603=CARTESIAN_POINT ( 'NONE',  ( 16.13393739769620083, -15.61618894467929941, -6.189999999999999503 ) ) ;
#25606=VERTEX_POINT ( 'NONE', #12902 ) ;
#25611=CARTESIAN_POINT ( 'NONE',  ( 3.133937397696200389, -15.61618894467929763, -6.189999999999999503 ) ) ;
#25614=TOROIDAL_SURFACE ( 'NONE', #6418, 12.50000000000000000, 1.000000000000000000 ) ;
#25641=AXIS2_PLACEMENT_3D ( 'NONE', #38650, #10347, #34947 ) ;
#25653=AXIS2_PLACEMENT_3D ( 'NONE', #33057, #40420, #28351 ) ;
#25655=DIRECTION ( 'NONE',  ( 0.000000000000000000, 0.000000000000000000, 1.000000000000000000 ) ) ;
#25660=ORIENTED_EDGE ( 'NONE', *, *, #10048, .T. ) ;
#25697=AXIS2_PLACEMENT_3D ( 'NONE', #8469, #48299, #25203 ) ;
#25755=ORIENTED_EDGE ( 'NONE', *, *, #20342, .T. ) ;
#25768=AXIS2_PLACEMENT_3D ( 'NONE', #2089, #2343, #18317 ) ;
#25788=FACE_OUTER_BOUND ( 'NONE', #16635, .T. ) ;
#25827=AXIS2_PLACEMENT_3D ( 'NONE', #9813, #49395, #9556 ) ;
#25854=ADVANCED_FACE ( 'NONE', ( #9356 ), #2510, .F. ) ;
#25859=CARTESIAN_POINT ( 'NONE',  ( 16.13393739769620083, -15.61618894467929941, -18.58999999999999986 ) ) ;
#25872=AXIS2_PLACEMENT_3D ( 'NONE', #46783, #30503, #11644 ) ;
#25883=DIRECTION ( 'NONE',  ( 1.000000000000000000, 0.000000000000000000, 0.000000000000000000 ) ) ;
#25888=EDGE_CURVE ( 'NONE', #28421, #39126, #2668, .T. ) ;
#25897=CARTESIAN_POINT ( 'NONE',  ( -30.36606260230379917, -53.11618894467940066, 17.35000000000000142 ) ) ;
#25904=AXIS2_PLACEMENT_3D ( 'NONE', #28407, #20284, #40225 ) ;
#25913=AXIS2_PLACEMENT_3D ( 'NONE', #41110, #48456, #12825 ) ;
#25929=ORIENTED_EDGE ( 'NONE', *, *, #5322, .T. ) ;
#25974=ORIENTED_EDGE ( 'NONE', *, *, #12785, .T. ) ;
#25987=DIRECTION ( 'NONE',  ( 0.000000000000000000, 0.000000000000000000, 1.000000000000000000 ) ) ;
#25995=CARTESIAN_POINT ( 'NONE',  ( 53.63393739769619373, -53.11618894467930119, 17.35000000000000142 ) ) ;
#26001=DIRECTION ( 'NONE',  ( 1.000000000000000000, 0.000000000000000000, 0.000000000000000000 ) ) ;
#26054=CYLINDRICAL_SURFACE ( 'NONE', #2214, 10.00000000000000711 ) ;
#26055=EDGE_LOOP ( 'NONE', ( #13540, #41048, #49454, #26645 ) ) ;
#26058=EDGE_CURVE ( 'NONE', #20782, #29727, #3504, .T. ) ;
#26073=ORIENTED_EDGE ( 'NONE', *, *, #45206, .T. ) ;
#26079=ORIENTED_EDGE ( 'NONE', *, *, #30788, .F. ) ;
#26084=VERTEX_POINT ( 'NONE', #8509 ) ;
#26093=CIRCLE ( 'NONE', #16084, 5.499999999999998224 ) ;
#26095=CIRCLE ( 'NONE', #21083, 4.649999999999999467 ) ;
#26098=CARTESIAN_POINT ( 'NONE',  ( -28.43713041416928178, 28.95487886718607839, 17.35000000000000142 ) ) ;
#26128=DIRECTION ( 'NONE',  ( 0.000000000000000000, 0.000000000000000000, -1.000000000000000000 ) ) ;
#26130=ORIENTED_EDGE ( 'NONE', *, *, #29395, .F. ) ;
#26133=CIRCLE ( 'NONE', #3565, 2.000000000000000000 ) ;
#26134=DIRECTION ( 'NONE',  ( 1.224646799147353207E-16, 1.000000000000000000, -0.000000000000000000 ) ) ;
#26136=CIRCLE ( 'NONE', #1049, 18.86180339887500068 ) ;
#26143=ADVANCED_FACE ( 'NONE', ( #33350, #48842 ), #24952, .T. ) ;
#26175=CARTESIAN_POINT ( 'NONE',  ( -18.86606260230390220, 19.38381105532060289, 11.34999999999999964 ) ) ;
#26200=DIRECTION ( 'NONE',  ( 0.000000000000000000, 0.000000000000000000, -1.000000000000000000 ) ) ;
#26228=EDGE_CURVE ( 'NONE', #29727, #20782, #13557, .T. ) ;
#26239=ORIENTED_EDGE ( 'NONE', *, *, #42884, .F. ) ;
#26246=AXIS2_PLACEMENT_3D ( 'NONE', #48968, #32674, #12535 ) ;
#26249=AXIS2_PLACEMENT_3D ( 'NONE', #15677, #12261, #51579 ) ;
#26253=DIRECTION ( 'NONE',  ( 0.000000000000000000, 0.000000000000000000, 1.000000000000000000 ) ) ;
#26258=CARTESIAN_POINT ( 'NONE',  ( -22.09888148991250389, 23.83340452438281076, 16.85000000000000142 ) ) ;
#26283=CARTESIAN_POINT ( 'NONE',  ( -30.36606260230379917, 21.88381105532059934, 10.84999999999999964 ) ) ;
#26304=DIRECTION ( 'NONE',  ( 1.000000000000000000, 0.000000000000000000, 0.000000000000000000 ) ) ;
#26332=ORIENTED_EDGE ( 'NONE', *, *, #32904, .F. ) ;
#26333=ORIENTED_EDGE ( 'NONE', *, *, #18025, .F. ) ;
#26339=CARTESIAN_POINT ( 'NONE',  ( 53.63393739769619373, 31.88381105532059934, 16.35000000000000142 ) ) ;
#26345=CARTESIAN_POINT ( 'NONE',  ( -18.86606260230360022, -50.61618894467959962, 11.34999999999999964 ) ) ;
#26355=SURFACE_STYLE_USAGE ( .BOTH. , #50237 ) ;
#26362=CIRCLE ( 'NONE', #29705, 13.50000000000000178 ) ;
#26375=CARTESIAN_POINT ( 'NONE',  ( 63.63393739769619373, -63.11618894467939356, 17.35000000000000142 ) ) ;
#26417=FACE_OUTER_BOUND ( 'NONE', #30395, .T. ) ;
#26421=EDGE_LOOP ( 'NONE', ( #28387, #46065 ) ) ;
#26423=CIRCLE ( 'NONE', #49058, 17.63819660112499932 ) ;
#26429=CARTESIAN_POINT ( 'NONE',  ( 53.63393739769619373, -62.11618894467930119, 17.35000000000000142 ) ) ;
#26461=EDGE_CURVE ( 'NONE', #35304, #29727, #8504, .T. ) ;
#26465=VERTEX_POINT ( 'NONE', #27813 ) ;
#26468=VERTEX_POINT ( 'NONE', #44319 ) ;
#26469=DIRECTION ( 'NONE',  ( 0.000000000000000000, -8.281569874363147012E-12, 1.000000000000000000 ) ) ;
#26474=DIRECTION ( 'NONE',  ( 0.000000000000000000, 0.000000000000000000, 1.000000000000000000 ) ) ;
#26491=DIRECTION ( 'NONE',  ( 1.000000000000000000, 0.000000000000000000, 0.000000000000000000 ) ) ;
#26509=CARTESIAN_POINT ( 'NONE',  ( -21.36606260230379917, 30.88381105532059934, 17.35000000000000142 ) ) ;
#26546=CARTESIAN_POINT ( 'NONE',  ( 0.000000000000000000, 0.000000000000000000, 0.000000000000000000 ) ) ;
#26582=CARTESIAN_POINT ( 'NONE',  ( -30.36606260230379917, 21.88381105532059934, 16.35000000000000142 ) ) ;
#26592=EDGE_CURVE ( 'NONE', #17966, #39558, #21873, .T. ) ;
#26596=ORIENTED_EDGE ( 'NONE', *, *, #16917, .F. ) ;
#26597=VERTEX_POINT ( 'NONE', #40363 ) ;
#26601=ORIENTED_EDGE ( 'NONE', *, *, #47296, .F. ) ;
#26632=ORIENTED_EDGE ( 'NONE', *, *, #37335, .F. ) ;
#26645=ORIENTED_EDGE ( 'NONE', *, *, #42884, .T. ) ;
#26650=EDGE_LOOP ( 'NONE', ( #12762, #27877, #34011, #19783 ) ) ;
#26662=VERTEX_POINT ( 'NONE', #37728 ) ;
#26669=ADVANCED_FACE ( 'NONE', ( #21466 ), #10188, .F. ) ;
#26675=CARTESIAN_POINT ( 'NONE',  ( 16.13393739769620083, -15.61618894467929941, -12.13039854958090125 ) ) ;
#26710=VERTEX_POINT ( 'NONE', #25391 ) ;
#26717=EDGE_CURVE ( 'NONE', #49517, #9988, #42180, .T. ) ;
#26732=CARTESIAN_POINT ( 'NONE',  ( -12.13714804906302369, -15.61618894467930119, 9.349999999999999645 ) ) ;
#26741=ORIENTED_EDGE ( 'NONE', *, *, #19551, .T. ) ;
#26747=CONICAL_SURFACE ( 'NONE', #37642, 0.6299999999999991163, 0.7853981633974490562 ) ;
#26751=DIRECTION ( 'NONE',  ( -0.4156269377774536311, 0.5720614028176836952, 0.7071067811865477948 ) ) ;
#26761=CARTESIAN_POINT ( 'NONE',  ( -3.866062602303799611, -15.61618894467929763, -18.58999999999999986 ) ) ;
#26812=DIRECTION ( 'NONE',  ( -1.000000000000000000, 0.000000000000000000, 0.000000000000000000 ) ) ;
#26819=DIRECTION ( 'NONE',  ( 0.000000000000000000, 0.000000000000000000, 1.000000000000000000 ) ) ;
#26860=AXIS2_PLACEMENT_3D ( 'NONE', #39613, #3716, #39870 ) ;
#26904=FACE_OUTER_BOUND ( 'NONE', #26650, .T. ) ;
#26914=CARTESIAN_POINT ( 'NONE',  ( -15.63324371469529694, 14.93421758625839857, 16.85000000000000142 ) ) ;
#26916=ORIENTED_EDGE ( 'NONE', *, *, #48245, .T. ) ;
#26923=ORIENTED_EDGE ( 'NONE', *, *, #41538, .F. ) ;
#26931=VECTOR ( 'NONE', #41848, 1000.000000000000000 ) ;
#26953=CARTESIAN_POINT ( 'NONE',  ( 51.13393739769659874, -50.61618894467899565, 16.21999999999999886 ) ) ;
#26968=CARTESIAN_POINT ( 'NONE',  ( -18.86606260230390220, 13.88381105532060289, 14.21249999999999858 ) ) ;
#26971=CARTESIAN_POINT ( 'NONE',  ( -18.86606260230390220, 13.88381105532060289, 11.34999999999999964 ) ) ;
#27016=CARTESIAN_POINT ( 'NONE',  ( 16.13393739769620083, -15.61618894467929941, -18.58999999999999986 ) ) ;
#27078=CIRCLE ( 'NONE', #33767, 5.499999999999998224 ) ;
#27080=ADVANCED_FACE ( 'NONE', ( #30497 ), #47457, .F. ) ;
#27099=DIRECTION ( 'NONE',  ( 0.000000000000000000, 0.000000000000000000, 1.000000000000000000 ) ) ;
#27121=DIRECTION ( 'NONE',  ( 1.000000000000000000, 0.000000000000000000, 0.000000000000000000 ) ) ;
#27126=ORIENTED_EDGE ( 'NONE', *, *, #10833, .T. ) ;
#27131=EDGE_LOOP ( 'NONE', ( #10900, #48243, #17345, #6170, #46945 ) ) ;
#27136=AXIS2_PLACEMENT_3D ( 'NONE', #19466, #18692, #6915 ) ;
#27150=CARTESIAN_POINT ( 'NONE',  ( 16.13393739769620083, -15.61618894467929941, -18.08174999999999955 ) ) ;
#27155=ORIENTED_EDGE ( 'NONE', *, *, #36010, .F. ) ;
#27162=DIRECTION ( 'NONE',  ( -2.066387465239710029E-12, 1.205421602240320019E-11, 1.000000000000000000 ) ) ;
#27172=VERTEX_POINT ( 'NONE', #3253 ) ;
#27188=ORIENTED_EDGE ( 'NONE', *, *, #3135, .T. ) ;
#27190=DIRECTION ( 'NONE',  ( 0.000000000000000000, -1.000000000000000000, 0.000000000000000000 ) ) ;
#27194=DIRECTION ( 'NONE',  ( 0.000000000000000000, 0.000000000000000000, 1.000000000000000000 ) ) ;
#27230=ORIENTED_EDGE ( 'NONE', *, *, #34515, .T. ) ;
#27238=EDGE_LOOP ( 'NONE', ( #12975, #22016, #25579, #22454, #44666, #176 ) ) ;
#27285=EDGE_LOOP ( 'NONE', ( #42138, #8454 ) ) ;
#27306=CARTESIAN_POINT ( 'NONE',  ( 16.13393739769609780, -15.61618894467929941, 7.919999999999999929 ) ) ;
#27309=ORIENTED_EDGE ( 'NONE', *, *, #44753, .F. ) ;
#27319=CONICAL_SURFACE ( 'NONE', #28128, 0.6405000000000011795, 1.029744258676660307 ) ;
#27324=CARTESIAN_POINT ( 'NONE',  ( 29.63393739769620083, -15.61618894467929941, -6.189999999999999503 ) ) ;
#27374=ORIENTED_EDGE ( 'NONE', *, *, #50099, .F. ) ;
#27382=EDGE_CURVE ( 'NONE', #4500, #39126, #51468, .T. ) ;
#27384=ORIENTED_EDGE ( 'NONE', *, *, #48099, .T. ) ;
#27386=DIRECTION ( 'NONE',  ( 1.000000000000000000, 0.000000000000000000, 0.000000000000000000 ) ) ;
#27404=EDGE_CURVE ( 'NONE', #46283, #20497, #45764, .T. ) ;
#27418=CARTESIAN_POINT ( 'NONE',  ( -18.86606260230390220, 19.38381105532060289, 11.97999999999999865 ) ) ;
#27419=DIRECTION ( 'NONE',  ( 0.000000000000000000, 1.000000000000000000, 0.000000000000000000 ) ) ;
#27420=CARTESIAN_POINT ( 'NONE',  ( 51.13393739769620083, 19.38381105532069881, 11.34999999999999964 ) ) ;
#27466=EDGE_CURVE ( 'NONE', #24630, #8804, #10640, .T. ) ;
#27471=CARTESIAN_POINT ( 'NONE',  ( 62.63393739769619373, 21.88381105532059934, 11.84999999999999964 ) ) ;
#27486=FACE_OUTER_BOUND ( 'NONE', #17405, .T. ) ;
#27489=VERTEX_POINT ( 'NONE', #25461 ) ;
#27498=VECTOR ( 'NONE', #37244, 1000.000000000000000 ) ;
#27505=ORIENTED_EDGE ( 'NONE', *, *, #12009, .T. ) ;
#27539=EDGE_CURVE ( 'NONE', #10341, #49525, #20759, .T. ) ;
#27551=FACE_OUTER_BOUND ( 'NONE', #45746, .T. ) ;
#27560=ADVANCED_FACE ( 'NONE', ( #8728 ), #44887, .T. ) ;
#27574=CONICAL_SURFACE ( 'NONE', #48534, 0.6299999999999866818, 0.7853981633974476129 ) ;
#27597=CARTESIAN_POINT ( 'NONE',  ( 16.13393739769620083, -15.61618894467929941, -6.189999999999999503 ) ) ;
#27598=CARTESIAN_POINT ( 'NONE',  ( 20.78393739769619941, -15.61618894467929941, -14.03562394879499919 ) ) ;
#27599=AXIS2_PLACEMENT_3D ( 'NONE', #6727, #50741, #14839 ) ;
#27603=TOROIDAL_SURFACE ( 'NONE', #10909, 9.000000000000000000, 1.000000000000000000 ) ;
#27628=EDGE_LOOP ( 'NONE', ( #16932, #48816, #29912, #17963, #51507, #18166 ) ) ;
#27635=VERTEX_POINT ( 'NONE', #46199 ) ;
#27641=AXIS2_PLACEMENT_3D ( 'NONE', #20922, #28263, #16228 ) ;
#27643=ORIENTED_EDGE ( 'NONE', *, *, #110, .T. ) ;
#27679=EDGE_CURVE ( 'NONE', #13493, #45801, #6352, .T. ) ;
#27683=DIRECTION ( 'NONE',  ( 0.000000000000000000, 0.000000000000000000, 1.000000000000000000 ) ) ;
#27695=CARTESIAN_POINT ( 'NONE',  ( 16.13393739769620083, -15.61618894467929941, 14.34999999999999964 ) ) ;
#27710=DIRECTION ( 'NONE',  ( 1.000000000000000000, 0.000000000000000000, 0.000000000000000000 ) ) ;
#27728=ADVANCED_FACE ( 'NONE', ( #42253 ), #19754, .F. ) ;
#27738=ORIENTED_EDGE ( 'NONE', *, *, #46272, .T. ) ;
#27741=DIRECTION ( 'NONE',  ( 0.000000000000000000, 1.000000000000000000, 0.000000000000000000 ) ) ;
#27769=EDGE_LOOP ( 'NONE', ( #14491, #37619, #35568, #2095 ) ) ;
#27777=CARTESIAN_POINT ( 'NONE',  ( 12.37200837385271868, -18.34939036783928046, -9.721247897589949005 ) ) ;
#27784=CARTESIAN_POINT ( 'NONE',  ( -20.36606260510179567, -15.61618894418049308, 9.349999998653533595 ) ) ;
#27813=CARTESIAN_POINT ( 'NONE',  ( -1.866062602303798723, -15.61618894467929763, -20.58999999999999986 ) ) ;
#27820=ORIENTED_EDGE ( 'NONE', *, *, #5685, .T. ) ;
#27850=ORIENTED_EDGE ( 'NONE', *, *, #29771, .F. ) ;
#27877=ORIENTED_EDGE ( 'NONE', *, *, #39185, .F. ) ;
#27884=CARTESIAN_POINT ( 'NONE',  ( -14.41646913324139589, -53.84900783228822263, 11.34999999999999964 ) ) ;
#27892=ORIENTED_EDGE ( 'NONE', *, *, #37070, .F. ) ;
#27893=AXIS2_PLACEMENT_3D ( 'NONE', #29484, #21608, #10104 ) ;
#27908=DIRECTION ( 'NONE',  ( 0.000000000000000000, -1.000000000000000000, 0.000000000000000000 ) ) ;
#27930=FACE_OUTER_BOUND ( 'NONE', #50252, .T. ) ;
#27933=DIRECTION ( 'NONE',  ( 1.000000000000000000, 0.000000000000000000, 0.000000000000000000 ) ) ;
#27971=EDGE_CURVE ( 'NONE', #18473, #10844, #4676, .T. ) ;
#27986=ORIENTED_EDGE ( 'NONE', *, *, #51184, .F. ) ;
#28016=ADVANCED_FACE ( 'NONE', ( #7645 ), #33124, .F. ) ;
#28023=AXIS2_PLACEMENT_3D ( 'NONE', #21132, #25315, #1492 ) ;
#28024=CARTESIAN_POINT ( 'NONE',  ( 16.13393739769620083, -15.61618894467929941, 17.35000000000000142 ) ) ;
#28030=DIRECTION ( 'NONE',  ( 0.7071067811865473507, 0.7071067811865476838, 0.000000000000000000 ) ) ;
#28056=CARTESIAN_POINT ( 'NONE',  ( 16.13393739769620083, -15.61618894467929941, -18.08174999999999955 ) ) ;
#28058=EDGE_LOOP ( 'NONE', ( #1439, #14488, #21972, #49394, #1419 ) ) ;
#28124=DIRECTION ( 'NONE',  ( -1.000000000000000000, 0.000000000000000000, 0.000000000000000000 ) ) ;
#28126=CARTESIAN_POINT ( 'NONE',  ( 5.633937397983799222, -15.61618894439989802, -19.08999999986939855 ) ) ;
#28128=AXIS2_PLACEMENT_3D ( 'NONE', #2164, #26253, #29918 ) ;
#28141=FACE_OUTER_BOUND ( 'NONE', #38751, .T. ) ;
#28153=DIRECTION ( 'NONE',  ( 0.000000000000000000, 0.000000000000000000, -1.000000000000000000 ) ) ;
#28156=AXIS2_PLACEMENT_3D ( 'NONE', #44375, #49356, #40954 ) ;
#28166=DIRECTION ( 'NONE',  ( -1.000000000000000000, 0.000000000000000000, 0.000000000000000000 ) ) ;
#28179=ORIENTED_EDGE ( 'NONE', *, *, #42299, .T. ) ;
#28192=ORIENTED_EDGE ( 'NONE', *, *, #42299, .F. ) ;
#28193=ORIENTED_EDGE ( 'NONE', *, *, #25246, .T. ) ;
#28194=DIRECTION ( 'NONE',  ( 0.7071067811865475727, -0.7071067811865475727, 0.000000000000000000 ) ) ;
#28216=DIRECTION ( 'NONE',  ( -1.000000000000000000, 0.000000000000000000, 0.000000000000000000 ) ) ;
#28235=FACE_OUTER_BOUND ( 'NONE', #36915, .T. ) ;
#28258=LINE ( 'NONE', #13093, #39931 ) ;
#28263=DIRECTION ( 'NONE',  ( 4.718060457820110146E-11, -8.281540456132319756E-12, 1.000000000000000000 ) ) ;
#28274=CARTESIAN_POINT ( 'NONE',  ( 21.38393739769620083, -15.61618894467929941, -18.58999999999999986 ) ) ;
#28284=DIRECTION ( 'NONE',  ( 5.878706999999999976E-17, 3.795112000000000086E-17, 1.000000000000000000 ) ) ;
#28287=DIRECTION ( 'NONE',  ( 0.000000000000000000, 0.000000000000000000, -1.000000000000000000 ) ) ;
#28289=CARTESIAN_POINT ( 'NONE',  ( 62.63393739769619373, 21.88381105532059934, 16.35000000000000142 ) ) ;
#28299=ADVANCED_FACE ( 'NONE', ( #25788 ), #26054, .T. ) ;
#28314=ORIENTED_EDGE ( 'NONE', *, *, #36077, .T. ) ;
#28344=AXIS2_PLACEMENT_3D ( 'NONE', #28473, #40539, #44472 ) ;
#28351=DIRECTION ( 'NONE',  ( 0.000000000000000000, 0.000000000000000000, -1.000000000000000000 ) ) ;
#28362=EDGE_LOOP ( 'NONE', ( #23268, #25021, #9743, #21489, #29296 ) ) ;
#28387=ORIENTED_EDGE ( 'NONE', *, *, #51512, .F. ) ;
#28389=VERTEX_POINT ( 'NONE', #38132 ) ;
#28400=DIRECTION ( 'NONE',  ( 0.000000000000000000, 0.000000000000000000, 1.000000000000000000 ) ) ;
#28404=EDGE_LOOP ( 'NONE', ( #410, #25929, #27643, #7259, #11457 ) ) ;
#28407=CARTESIAN_POINT ( 'NONE',  ( 51.13393739769620083, 19.38381105532069881, 17.35000000000000142 ) ) ;
#28415=CIRCLE ( 'NONE', #35981, 5.500000000000000000 ) ;
#28421=VERTEX_POINT ( 'NONE', #14024 ) ;
#28462=EDGE_LOOP ( 'NONE', ( #23529, #46351, #32766, #10784, #3854, #17816, #14145 ) ) ;
#28472=ORIENTED_EDGE ( 'NONE', *, *, #19390, .T. ) ;
#28473=CARTESIAN_POINT ( 'NONE',  ( 16.13393739769620083, -15.61618894467929941, -8.849999999999999645 ) ) ;
#28478=DIRECTION ( 'NONE',  ( 1.000000000000000000, 0.000000000000000000, 0.000000000000000000 ) ) ;
#28479=CARTESIAN_POINT ( 'NONE',  ( 3.633937397696199056, -15.61618894467929763, -1.149999999999999911 ) ) ;
#28487=CARTESIAN_POINT ( 'NONE',  ( 47.60722588394180121, -55.47029091092869635, 10.84999999999999964 ) ) ;
#28491=CARTESIAN_POINT ( 'NONE',  ( 16.13393739769620083, -15.61618894467929941, -16.88999999999999702 ) ) ;
#28516=FACE_OUTER_BOUND ( 'NONE', #1144, .T. ) ;
#28535=CARTESIAN_POINT ( 'NONE',  ( 16.13393739769620083, -15.61618894467929941, -18.58999999999999986 ) ) ;
#28536=LINE ( 'NONE', #20669, #38594 ) ;
#28557=CARTESIAN_POINT ( 'NONE',  ( 44.40502284445533832, -15.61618894467929763, 9.349999999999999645 ) ) ;
#28564=AXIS2_PLACEMENT_3D ( 'NONE', #49368, #45427, #25480 ) ;
#28588=ORIENTED_EDGE ( 'NONE', *, *, #37281, .F. ) ;
#28591=ORIENTED_EDGE ( 'NONE', *, *, #50569, .F. ) ;
#28615=EDGE_LOOP ( 'NONE', ( #50528, #46132, #46361, #12237 ) ) ;
#28621=EDGE_CURVE ( 'NONE', #50052, #51387, #39892, .T. ) ;
#28647=ORIENTED_EDGE ( 'NONE', *, *, #18490, .F. ) ;
#28657=CARTESIAN_POINT ( 'NONE',  ( 16.13393739769620083, -15.61618894467929941, -15.18999999999999950 ) ) ;
#28665=ADVANCED_FACE ( 'NONE', ( #9967 ), #42984, .T. ) ;
#28712=DIRECTION ( 'NONE',  ( 0.000000000000000000, 0.000000000000000000, 1.000000000000000000 ) ) ;
#28719=ORIENTED_EDGE ( 'NONE', *, *, #14566, .T. ) ;
#28752=CIRCLE ( 'NONE', #48874, 9.999999999999998224 ) ;
#28759=DIRECTION ( 'NONE',  ( 0.000000000000000000, 0.000000000000000000, 1.000000000000000000 ) ) ;
#28761=EDGE_LOOP ( 'NONE', ( #3485, #2501 ) ) ;
#28774=CIRCLE ( 'NONE', #2914, 0.9999999999999974465 ) ;
#28785=VERTEX_POINT ( 'NONE', #17825 ) ;
#28788=CIRCLE ( 'NONE', #30478, 1.000000000000000888 ) ;
#28801=LINE ( 'NONE', #5239, #11294 ) ;
#28809=CIRCLE ( 'NONE', #27136, 0.9999999999999974465 ) ;
#28811=CARTESIAN_POINT ( 'NONE',  ( 16.13393739769620083, -15.61618894467929941, 2.750000000000000000 ) ) ;
#28815=FACE_OUTER_BOUND ( 'NONE', #11206, .T. ) ;
#28816=DIRECTION ( 'NONE',  ( 0.000000000000000000, 0.000000000000000000, 1.000000000000000000 ) ) ;
#28818=FACE_OUTER_BOUND ( 'NONE', #2733, .T. ) ;
#28837=CARTESIAN_POINT ( 'NONE',  ( 16.13393739566809870, -15.61618894418049841, 9.349999999609689638 ) ) ;
#28869=EDGE_CURVE ( 'NONE', #31144, #18163, #13933, .T. ) ;
#28879=ORIENTED_EDGE ( 'NONE', *, *, #13735, .F. ) ;
#28917=CARTESIAN_POINT ( 'NONE',  ( 16.13393739769620083, -15.61618894467929941, -9.721247897589949005 ) ) ;
#28918=VERTEX_POINT ( 'NONE', #19632 ) ;
#28922=ORIENTED_EDGE ( 'NONE', *, *, #39208, .F. ) ;
#28997=AXIS2_PLACEMENT_3D ( 'NONE', #11069, #23338, #19173 ) ;
#29005=DIRECTION ( 'NONE',  ( 0.000000000000000000, 0.000000000000000000, -1.000000000000000000 ) ) ;
#29006=ADVANCED_FACE ( 'NONE', ( #27486 ), #47684, .T. ) ;
#29020=CARTESIAN_POINT ( 'NONE',  ( -21.36606260230379917, -62.11618894467930119, 16.35000000000000142 ) ) ;
#29038=EDGE_CURVE ( 'NONE', #50796, #25606, #20548, .T. ) ;
#29040=DIRECTION ( 'NONE',  ( -0.7071067811865476838, -0.7071067811865473507, 0.000000000000000000 ) ) ;
#29042=ORIENTED_EDGE ( 'NONE', *, *, #19288, .F. ) ;
#29059=DIRECTION ( 'NONE',  ( 0.000000000000000000, -1.000000000000000000, 0.000000000000000000 ) ) ;
#29062=DIRECTION ( 'NONE',  ( 0.000000000000000000, -1.000000000000000000, 0.000000000000000000 ) ) ;
#29075=ADVANCED_FACE ( 'NONE', ( #28516 ), #7190, .F. ) ;
#29078=FACE_OUTER_BOUND ( 'NONE', #25550, .T. ) ;
#29094=ADVANCED_FACE ( 'NONE', ( #17007 ), #24831, .T. ) ;
#29107=DIRECTION ( 'NONE',  ( 0.4156269377774486906, 0.5720614028176872479, -0.7071067811865479058 ) ) ;
#29154=FACE_OUTER_BOUND ( 'NONE', #27131, .T. ) ;
#29156=DIRECTION ( 'NONE',  ( -0.7071067811865470176, 0.000000000000000000, 0.7071067811865480168 ) ) ;
#29179=ORIENTED_EDGE ( 'NONE', *, *, #6688, .F. ) ;
#29187=VERTEX_POINT ( 'NONE', #33221 ) ;
#29207=CIRCLE ( 'NONE', #39262, 4.999999999969890752 ) ;
#29209=ADVANCED_FACE ( 'NONE', ( #37947 ), #10689, .F. ) ;
#29216=ORIENTED_EDGE ( 'NONE', *, *, #47575, .F. ) ;
#29226=DIRECTION ( 'NONE',  ( 0.000000000000000000, -1.000000000000000000, 0.000000000000000000 ) ) ;
#29237=CYLINDRICAL_SURFACE ( 'NONE', #22506, 1.000000000000001332 ) ;
#29261=EDGE_CURVE ( 'NONE', #49525, #11148, #34779, .T. ) ;
#29274=CARTESIAN_POINT ( 'NONE',  ( -18.86606260230390220, 24.88381105532059934, 14.21249999999999858 ) ) ;
#29295=VERTEX_POINT ( 'NONE', #50002 ) ;
#29296=ORIENTED_EDGE ( 'NONE', *, *, #30553, .F. ) ;
#29319=EDGE_CURVE ( 'NONE', #51110, #34913, #38461, .T. ) ;
#29368=EDGE_CURVE ( 'NONE', #22408, #17966, #50732, .T. ) ;
#29377=DIRECTION ( 'NONE',  ( 0.000000000000000000, 0.000000000000000000, 1.000000000000000000 ) ) ;
#29382=CARTESIAN_POINT ( 'NONE',  ( 16.13393739769609780, -15.61618894467929941, 7.919999999999999929 ) ) ;
#29395=EDGE_CURVE ( 'NONE', #40267, #51110, #3861, .T. ) ;
#29400=LINE ( 'NONE', #36477, #30620 ) ;
#29433=LINE ( 'NONE', #49889, #19487 ) ;
#29441=DIRECTION ( 'NONE',  ( -1.000000000000000000, 0.000000000000000000, 0.000000000000000000 ) ) ;
#29462=DIRECTION ( 'NONE',  ( 1.000000000000000000, 0.000000000000000000, 0.000000000000000000 ) ) ;
#29476=DIRECTION ( 'NONE',  ( 0.000000000000000000, 0.000000000000000000, -1.000000000000000000 ) ) ;
#29477=VERTEX_POINT ( 'NONE', #26914 ) ;
#29484=CARTESIAN_POINT ( 'NONE',  ( 62.63393739769619373, 21.88381105532059934, 16.35000000000000142 ) ) ;
#29491=ORIENTED_EDGE ( 'NONE', *, *, #37633, .T. ) ;
#29558=ORIENTED_EDGE ( 'NONE', *, *, #20657, .F. ) ;
#29560=DIRECTION ( 'NONE',  ( -2.840828347717470042E-11, 6.470619327693540153E-12, 1.000000000000000000 ) ) ;
#29561=CIRCLE ( 'NONE', #46355, 10.27649999999999864 ) ;
#29580=AXIS2_PLACEMENT_3D ( 'NONE', #49991, #10419, #10679 ) ;
#29591=VECTOR ( 'NONE', #16234, 1000.000000000000000 ) ;
#29604=DIRECTION ( 'NONE',  ( 0.3618033988749886909, 0.2628655560595663521, 0.8944271909999162995 ) ) ;
#29623=EDGE_CURVE ( 'NONE', #31353, #28785, #44891, .T. ) ;
#29627=CARTESIAN_POINT ( 'NONE',  ( 16.13393739566809870, -15.61618894418049841, 9.349999999609689638 ) ) ;
#29645=VECTOR ( 'NONE', #24417, 1000.000000000000000 ) ;
#29675=ORIENTED_EDGE ( 'NONE', *, *, #19847, .T. ) ;
#29681=AXIS2_PLACEMENT_3D ( 'NONE', #41582, #18508, #21644 ) ;
#29687=ORIENTED_EDGE ( 'NONE', *, *, #4891, .F. ) ;
#29705=AXIS2_PLACEMENT_3D ( 'NONE', #31056, #47080, #39200 ) ;
#29710=EDGE_CURVE ( 'NONE', #24630, #28785, #29400, .T. ) ;
#29723=DIRECTION ( 'NONE',  ( 0.000000000000000000, 0.000000000000000000, -1.000000000000000000 ) ) ;
#29724=DIRECTION ( 'NONE',  ( 0.5720614028176865817, 0.4156269377774496343, 0.7071067811865480168 ) ) ;
#29727=VERTEX_POINT ( 'NONE', #34355 ) ;
#29749=ORIENTED_EDGE ( 'NONE', *, *, #31496, .F. ) ;
#29767=DIRECTION ( 'NONE',  ( 0.000000000000000000, 1.000000000000000000, 0.000000000000000000 ) ) ;
#29771=EDGE_CURVE ( 'NONE', #50414, #5441, #16419, .T. ) ;
#29809=DIRECTION ( 'NONE',  ( 1.000000000000000000, 0.000000000000000000, 0.000000000000000000 ) ) ;
#29835=EDGE_CURVE ( 'NONE', #23688, #14490, #8043, .T. ) ;
#29860=ORIENTED_EDGE ( 'NONE', *, *, #24455, .F. ) ;
#29876=VERTEX_POINT ( 'NONE', #50552 ) ;
#29878=CYLINDRICAL_SURFACE ( 'NONE', #48643, 20.00000000000000000 ) ;
#29884=FACE_BOUND ( 'NONE', #35512, .T. ) ;
#29896=ADVANCED_FACE ( 'NONE', ( #13874 ), #34814, .F. ) ;
#29899=FACE_OUTER_BOUND ( 'NONE', #17648, .T. ) ;
#29912=ORIENTED_EDGE ( 'NONE', *, *, #18378, .F. ) ;
#29918=DIRECTION ( 'NONE',  ( -0.8090169943749477843, -0.5877852522924728040, 0.000000000000000000 ) ) ;
#29928=CARTESIAN_POINT ( 'NONE',  ( 16.13393739769620083, -15.61618894467929941, -5.690000000000000391 ) ) ;
#29984=ORIENTED_EDGE ( 'NONE', *, *, #23679, .F. ) ;
#29994=CARTESIAN_POINT ( 'NONE',  ( 16.13393739769620083, -15.61618894467929941, 4.349999999999999645 ) ) ;
#30007=ORIENTED_EDGE ( 'NONE', *, *, #32623, .F. ) ;
#30021=DIRECTION ( 'NONE',  ( 1.000000000000000000, 0.000000000000000000, 0.000000000000000000 ) ) ;
#30032=UNCERTAINTY_MEASURE_WITH_UNIT (LENGTH_MEASURE( 1.000000000000000082E-05 ), #38433, 'distance_accuracy_value', 'NONE');
#30044=DIRECTION ( 'NONE',  ( 0.000000000000000000, 1.000000000000000000, 0.000000000000000000 ) ) ;
#30059=CIRCLE ( 'NONE', #20035, 9.000000000000007105 ) ;
#30062=AXIS2_PLACEMENT_3D ( 'NONE', #15744, #47722, #11826 ) ;
#30103=CIRCLE ( 'NONE', #33471, 0.9999999999999974465 ) ;
#30105=CARTESIAN_POINT ( 'NONE',  ( 16.13393739846139852, -15.61618894397629909, 14.85000000048049884 ) ) ;
#30110=AXIS2_PLACEMENT_3D ( 'NONE', #14938, #42994, #39062 ) ;
#30140=DIRECTION ( 'NONE',  ( 1.000000000000000000, 5.495516945195724241E-29, 2.619602780254359830E-11 ) ) ;
#30142=CARTESIAN_POINT ( 'NONE',  ( 27.13393739752232392, -15.61618894439989980, -19.08999999999999986 ) ) ;
#30152=DIRECTION ( 'NONE',  ( 0.000000000000000000, 0.000000000000000000, -1.000000000000000000 ) ) ;
#30165=EDGE_CURVE ( 'NONE', #17783, #41343, #24273, .T. ) ;
#30215=VERTEX_POINT ( 'NONE', #28487 ) ;
#30241=CARTESIAN_POINT ( 'NONE',  ( -0.9360626036098995684, -15.61618894434099758, -11.12000000062922922 ) ) ;
#30271=ORIENTED_EDGE ( 'NONE', *, *, #8513, .F. ) ;
#30277=ORIENTED_EDGE ( 'NONE', *, *, #11071, .F. ) ;
#30307=ORIENTED_EDGE ( 'NONE', *, *, #32241, .F. ) ;
#30361=DIRECTION ( 'NONE',  ( -1.000000000000000000, 0.000000000000000000, 0.000000000000000000 ) ) ;
#30395=EDGE_LOOP ( 'NONE', ( #7819, #27188, #44746, #24079, #37567, #44708, #15141 ) ) ;
#30396=EDGE_CURVE ( 'NONE', #3068, #26084, #45525, .T. ) ;
#30412=DIRECTION ( 'NONE',  ( 1.000000000000000000, 0.000000000000000000, 0.000000000000000000 ) ) ;
#30428=EDGE_CURVE ( 'NONE', #9988, #13604, #13439, .T. ) ;
#30471=ORIENTED_EDGE ( 'NONE', *, *, #19585, .T. ) ;
#30477=CARTESIAN_POINT ( 'NONE',  ( -18.86606260230380272, -15.61618894417760117, 9.349999999999999645 ) ) ;
#30478=AXIS2_PLACEMENT_3D ( 'NONE', #42317, #10346, #26304 ) ;
#30493=EDGE_CURVE ( 'NONE', #8620, #25307, #12600, .T. ) ;
#30497=FACE_OUTER_BOUND ( 'NONE', #44917, .T. ) ;
#30503=DIRECTION ( 'NONE',  ( 1.000000000000000000, 0.000000000000000000, 0.000000000000000000 ) ) ;
#30511=AXIS2_PLACEMENT_3D ( 'NONE', #38727, #2296, #6234 ) ;
#30538=AXIS2_PLACEMENT_3D ( 'NONE', #7704, #19737, #15807 ) ;
#30553=EDGE_CURVE ( 'NONE', #35579, #21555, #23705, .T. ) ;
#30571=DIRECTION ( 'NONE',  ( 1.000000000000000000, 0.000000000000000000, 0.000000000000000000 ) ) ;
#30574=FACE_OUTER_BOUND ( 'NONE', #7785, .T. ) ;
#30582=EDGE_CURVE ( 'NONE', #25261, #27489, #42312, .T. ) ;
#30589=EDGE_LOOP ( 'NONE', ( #29749, #37805, #38373, #47325 ) ) ;
#30591=CARTESIAN_POINT ( 'NONE',  ( 16.13393739769620083, -15.61618894467929941, -18.10000000000000142 ) ) ;
#30599=VERTEX_POINT ( 'NONE', #3302 ) ;
#30603=CONICAL_SURFACE ( 'NONE', #17229, 1.980489356881870222, 0.4636476090008052053 ) ;
#30620=VECTOR ( 'NONE', #45401, 1000.000000000000000 ) ;
#30631=EDGE_LOOP ( 'NONE', ( #6055, #17290 ) ) ;
#30633=TOROIDAL_SURFACE ( 'NONE', #2196, 18.49999999936520112, 4.999999999969890752 ) ;
#30650=DIRECTION ( 'NONE',  ( 1.000000000000000000, 0.000000000000000000, 0.000000000000000000 ) ) ;
#30679=CIRCLE ( 'NONE', #25653, 1.000000000000000888 ) ;
#30696=CARTESIAN_POINT ( 'NONE',  ( 51.13393739769620083, 19.38381105532069881, 16.21999999999999886 ) ) ;
#30717=AXIS2_PLACEMENT_3D ( 'NONE', #26375, #6489, #27419 ) ;
#30727=CARTESIAN_POINT ( 'NONE',  ( 8.043767453946731649, -21.49404146760402767, -5.966499999999999915 ) ) ;
#30761=CARTESIAN_POINT ( 'NONE',  ( 51.13393739769620083, 19.38381105532069881, 16.85000000000000142 ) ) ;
#30778=EDGE_LOOP ( 'NONE', ( #11663, #4879 ) ) ;
#30779=ORIENTED_EDGE ( 'NONE', *, *, #35198, .T. ) ;
#30788=EDGE_CURVE ( 'NONE', #16420, #6443, #25558, .T. ) ;
#30807=EDGE_CURVE ( 'NONE', #17993, #46283, #10855, .T. ) ;
#30813=DIRECTION ( 'NONE',  ( 0.000000000000000000, 0.000000000000000000, 1.000000000000000000 ) ) ;
#30823=DIRECTION ( 'NONE',  ( 0.000000000000000000, 0.000000000000000000, -1.000000000000000000 ) ) ;
#30825=CARTESIAN_POINT ( 'NONE',  ( 16.13393739769620083, -15.61618894467929941, 9.349999999999999645 ) ) ;
#30826=FACE_OUTER_BOUND ( 'NONE', #45499, .T. ) ;
#30841=CARTESIAN_POINT ( 'NONE',  ( 63.63393739769619373, 21.88381105532059934, 11.84999999999999964 ) ) ;
#30880=DIRECTION ( 'NONE',  ( 0.000000000000000000, -1.000000000000000000, 0.000000000000000000 ) ) ;
#30884=ORIENTED_EDGE ( 'NONE', *, *, #47470, .F. ) ;
#30885=AXIS2_PLACEMENT_3D ( 'NONE', #30996, #39144, #15291 ) ;
#30891=CIRCLE ( 'NONE', #35959, 0.5000000000000004441 ) ;
#30911=ORIENTED_EDGE ( 'NONE', *, *, #21041, .F. ) ;
#30936=AXIS2_PLACEMENT_3D ( 'NONE', #9841, #33922, #41802 ) ;
#30996=CARTESIAN_POINT ( 'NONE',  ( 16.13393739769620083, 30.88381105532059934, 11.84999999999999964 ) ) ;
#31007=DIRECTION ( 'NONE',  ( -0.3618033988749886909, -0.2628655560595661855, 0.8944271909999162995 ) ) ;
#31030=CARTESIAN_POINT ( 'NONE',  ( 53.63393739769619373, -53.11618894467930119, 17.35000000000000142 ) ) ;
#31041=CARTESIAN_POINT ( 'NONE',  ( -31.36606260230380272, 21.88381105532059934, 16.35000000000000142 ) ) ;
#31044=VECTOR ( 'NONE', #40209, 1000.000000000000000 ) ;
#31046=EDGE_CURVE ( 'NONE', #2118, #27635, #41199, .T. ) ;
#31056=CARTESIAN_POINT ( 'NONE',  ( 16.13393739769620083, -15.61618894467929941, -11.11999999999999922 ) ) ;
#31082=DIRECTION ( 'NONE',  ( 1.000000000000000000, 0.000000000000000000, 0.000000000000000000 ) ) ;
#31113=DIRECTION ( 'NONE',  ( 0.000000000000000000, -1.000000000000000000, 0.000000000000000000 ) ) ;
#31119=CARTESIAN_POINT ( 'NONE',  ( 16.13393739769620083, -15.61618894467929941, -14.68999999999999950 ) ) ;
#31144=VERTEX_POINT ( 'NONE', #2338 ) ;
#31167=ORIENTED_EDGE ( 'NONE', *, *, #37132, .T. ) ;
#31183=AXIS2_PLACEMENT_3D ( 'NONE', #10914, #22679, #42361 ) ;
#31187=DIRECTION ( 'NONE',  ( 1.000000000000000000, 0.000000000000000000, 0.000000000000000000 ) ) ;
#31209=ADVANCED_FACE ( 'NONE', ( #43217 ), #49701, .F. ) ;
#31231=EDGE_LOOP ( 'NONE', ( #11928, #47483, #33938, #43006 ) ) ;
#31235=VERTEX_POINT ( 'NONE', #3381 ) ;
#31251=CARTESIAN_POINT ( 'NONE',  ( -21.36606260230379917, 21.88381105532059934, 11.84999999999999964 ) ) ;
#31296=ORIENTED_EDGE ( 'NONE', *, *, #6734, .F. ) ;
#31307=EDGE_CURVE ( 'NONE', #16677, #28918, #12806, .T. ) ;
#31309=AXIS2_PLACEMENT_3D ( 'NONE', #46955, #38041, #22546 ) ;
#31318=( NAMED_UNIT ( * ) SI_UNIT ( $, .STERADIAN. ) SOLID_ANGLE_UNIT ( ) );
#31319=COLOUR_RGB ( '', 0.09019608, 0.27058824, 0.51372549) ;
#31346=EDGE_LOOP ( 'NONE', ( #9392, #42077, #23787, #24250 ) ) ;
#31353=VERTEX_POINT ( 'NONE', #47658 ) ;
#31372=DIRECTION ( 'NONE',  ( 0.000000000000000000, -1.000000000000000000, 0.000000000000000000 ) ) ;
#31373=ADVANCED_FACE ( 'NONE', ( #25328, #4650 ), #16984, .T. ) ;
#31380=CONICAL_SURFACE ( 'NONE', #25548, 1.980489356881870222, 0.4636476090008052053 ) ;
#31401=CYLINDRICAL_SURFACE ( 'NONE', #4461, 5.499999999999998224 ) ;
#31414=DIRECTION ( 'NONE',  ( 0.000000000000000000, -6.470469973722704271E-12, -1.000000000000000000 ) ) ;
#31416=ORIENTED_EDGE ( 'NONE', *, *, #20618, .T. ) ;
#31418=AXIS2_PLACEMENT_3D ( 'NONE', #29020, #25066, #720 ) ;
#31439=CARTESIAN_POINT ( 'NONE',  ( 16.13393739769620083, -15.61618894467929941, -16.68902128623620129 ) ) ;
#31473=DIRECTION ( 'NONE',  ( 0.000000000000000000, 0.000000000000000000, -1.000000000000000000 ) ) ;
#31492=AXIS2_PLACEMENT_3D ( 'NONE', #2354, #18595, #38789 ) ;
#31496=EDGE_CURVE ( 'NONE', #8898, #19834, #16707, .T. ) ;
#31558=EDGE_CURVE ( 'NONE', #50249, #16294, #6710, .T. ) ;
#31561=EDGE_CURVE ( 'NONE', #434, #46863, #5026, .T. ) ;
#31566=ADVANCED_FACE ( 'NONE', ( #46057 ), #21652, .T. ) ;
#31571=CARTESIAN_POINT ( 'NONE',  ( 26.13393739769619728, -15.61618894467929941, 17.35000000000000142 ) ) ;
#31583=CARTESIAN_POINT ( 'NONE',  ( 6.633937397696199945, -15.61618894467929941, -18.35000000000000142 ) ) ;
#31606=CARTESIAN_POINT ( 'NONE',  ( 16.13393739769620083, -15.61618894467929941, -2.149999999999999911 ) ) ;
#31623=CARTESIAN_POINT ( 'NONE',  ( -3.366062602303800055, -15.61618894467929763, -14.68999999999999950 ) ) ;
#31654=DIRECTION ( 'NONE',  ( -1.000000000000000000, 0.000000000000000000, 0.000000000000000000 ) ) ;
#31686=ADVANCED_FACE ( 'NONE', ( #41590 ), #21913, .T. ) ;
#31694=FACE_OUTER_BOUND ( 'NONE', #33006, .T. ) ;
#31697=CARTESIAN_POINT ( 'NONE',  ( 63.34104417888273986, 21.88381105532059934, 17.05710678118654755 ) ) ;
#31742=TOROIDAL_SURFACE ( 'NONE', #13372, 18.00000000000000000, 2.000000000000000000 ) ;
#31756=SHAPE_REPRESENTATION_RELATIONSHIP ( 'NONE' , 'NONE' ,  #4374, #33546 ) ;
#31776=CIRCLE ( 'NONE', #5034, 0.5000000000000000000 ) ;
#31795=EDGE_LOOP ( 'NONE', ( #29687, #9011, #21574, #14269, #25012 ) ) ;
#31803=EDGE_LOOP ( 'NONE', ( #33068, #26632 ) ) ;
#31846=EDGE_CURVE ( 'NONE', #31144, #17783, #45636, .T. ) ;
#31863=ORIENTED_EDGE ( 'NONE', *, *, #3906, .T. ) ;
#31899=DIRECTION ( 'NONE',  ( 0.000000000000000000, 0.000000000000000000, -1.000000000000000000 ) ) ;
#31913=DIRECTION ( 'NONE',  ( 0.000000000000000000, 0.000000000000000000, 1.000000000000000000 ) ) ;
#31922=EDGE_LOOP ( 'NONE', ( #10884, #21168, #23296, #36747, #28193 ) ) ;
#31989=DIRECTION ( 'NONE',  ( -1.000000000000000000, 0.000000000000000000, 0.000000000000000000 ) ) ;
#31993=EDGE_LOOP ( 'NONE', ( #34215, #33426, #50596, #12638, #10168 ) ) ;
#32045=CARTESIAN_POINT ( 'NONE',  ( -18.86606260230360022, -50.61618894467959962, 14.21249999999999858 ) ) ;
#32048=DIRECTION ( 'NONE',  ( 1.224647048234162108E-16, 1.000000000000000000, -1.205421602240320019E-11 ) ) ;
#32067=ORIENTED_EDGE ( 'NONE', *, *, #43960, .F. ) ;
#32076=CARTESIAN_POINT ( 'NONE',  ( -21.36606260230379917, 21.88381105532059934, 17.35000000000000142 ) ) ;
#32081=EDGE_LOOP ( 'NONE', ( #13772, #42996, #27126, #4343 ) ) ;
#32092=CARTESIAN_POINT ( 'NONE',  ( -18.86606260230390220, 19.38381105532060289, 10.84999999999999964 ) ) ;
#32107=LINE ( 'NONE', #45234, #6909 ) ;
#32125=CARTESIAN_POINT ( 'NONE',  ( 51.13393739769659874, -45.11618894467899565, 14.21249999999999858 ) ) ;
#32139=ADVANCED_FACE ( 'NONE', ( #17288 ), #44279, .F. ) ;
#32161=ORIENTED_EDGE ( 'NONE', *, *, #20482, .T. ) ;
#32173=AXIS2_PLACEMENT_3D ( 'NONE', #39482, #19548, #36556 ) ;
#32181=FACE_OUTER_BOUND ( 'NONE', #15470, .T. ) ;
#32197=VECTOR ( 'NONE', #16971, 1000.000000000000000 ) ;
#32204=CARTESIAN_POINT ( 'NONE',  ( 16.13393739769620083, -15.61618894467929941, -18.10000000000000142 ) ) ;
#32220=ORIENTED_EDGE ( 'NONE', *, *, #20093, .T. ) ;
#32231=CIRCLE ( 'NONE', #51505, 10.00000000000000711 ) ;
#32233=CARTESIAN_POINT ( 'NONE',  ( 62.63393739769619373, -63.11618894467939356, 11.84999999999999964 ) ) ;
#32241=EDGE_CURVE ( 'NONE', #24197, #8577, #18779, .T. ) ;
#32243=AXIS2_PLACEMENT_3D ( 'NONE', #12987, #44678, #9043 ) ;
#32252=CARTESIAN_POINT ( 'NONE',  ( 16.13393739769620083, -15.61618894467929941, 4.349999999999999645 ) ) ;
#32268=AXIS2_PLACEMENT_3D ( 'NONE', #30105, #42447, #2607 ) ;
#32368=EDGE_CURVE ( 'NONE', #35847, #4500, #35454, .T. ) ;
#32391=ADVANCED_FACE ( 'NONE', ( #19413 ), #48684, .T. ) ;
#32395=CARTESIAN_POINT ( 'NONE',  ( 16.13393739769620083, -15.61618894467929941, 2.750000000000000000 ) ) ;
#32405=CIRCLE ( 'NONE', #642, 5.499999999999998224 ) ;
#32412=FACE_OUTER_BOUND ( 'NONE', #39321, .T. ) ;
#32417=DIRECTION ( 'NONE',  ( -1.000000000000000000, 0.000000000000000000, 0.000000000000000000 ) ) ;
#32419=LINE ( 'NONE', #7588, #39647 ) ;
#32434=CYLINDRICAL_SURFACE ( 'NONE', #25913, 1.000000000000003775 ) ;
#32442=VERTEX_POINT ( 'NONE', #51137 ) ;
#32475=VECTOR ( 'NONE', #29107, 1000.000000000000114 ) ;
#32483=CIRCLE ( 'NONE', #17525, 5.499999999999998224 ) ;
#32501=EDGE_LOOP ( 'NONE', ( #2660, #2307, #9454, #12431, #21506 ) ) ;
#32507=ADVANCED_FACE ( 'NONE', ( #31694 ), #11823, .T. ) ;
#32545=CARTESIAN_POINT ( 'NONE',  ( -18.86606260230390220, 19.38381105532060289, 16.85000000000000142 ) ) ;
#32578=VERTEX_POINT ( 'NONE', #13366 ) ;
#32615=CARTESIAN_POINT ( 'NONE',  ( 47.90111851008797572, -46.16659547561683041, 16.85000000000000142 ) ) ;
#32623=EDGE_CURVE ( 'NONE', #1782, #6044, #39601, .T. ) ;
#32637=AXIS2_PLACEMENT_3D ( 'NONE', #29382, #826, #9491 ) ;
#32640=DIRECTION ( 'NONE',  ( 1.000000000000000000, 0.000000000000000000, 0.000000000000000000 ) ) ;
#32674=DIRECTION ( 'NONE',  ( 0.000000000000000000, -1.000000000000000000, 0.000000000000000000 ) ) ;
#32676=ORIENTED_EDGE ( 'NONE', *, *, #20808, .F. ) ;
#32694=LINE ( 'NONE', #487, #42446 ) ;
#32705=EDGE_LOOP ( 'NONE', ( #43522, #2887, #37653, #24784, #34303, #11721 ) ) ;
#32766=ORIENTED_EDGE ( 'NONE', *, *, #18025, .T. ) ;
#32799=DIRECTION ( 'NONE',  ( 0.000000000000000000, 0.000000000000000000, -1.000000000000000000 ) ) ;
#32800=VERTEX_POINT ( 'NONE', #50903 ) ;
#32843=CARTESIAN_POINT ( 'NONE',  ( 51.13393739769620083, 19.38381105532069881, 16.85000000000000142 ) ) ;
#32844=CARTESIAN_POINT ( 'NONE',  ( 27.13393739769620083, -15.61618894467929941, -20.58999999999999986 ) ) ;
#32872=EDGE_CURVE ( 'NONE', #6443, #16420, #46313, .T. ) ;
#32887=EDGE_LOOP ( 'NONE', ( #21364, #25755, #18032, #5155, #23542 ) ) ;
#32904=EDGE_CURVE ( 'NONE', #1082, #26468, #14507, .T. ) ;
#32941=DIRECTION ( 'NONE',  ( 1.735698870208309265E-22, -1.000000000000000000, 1.376914871200490071E-11 ) ) ;
#32945=ORIENTED_EDGE ( 'NONE', *, *, #6270, .F. ) ;
#32963=VERTEX_POINT ( 'NONE', #37240 ) ;
#32973=CARTESIAN_POINT ( 'NONE',  ( 16.13393739769620083, 31.59091783650714547, 11.14289321881345174 ) ) ;
#32976=FACE_BOUND ( 'NONE', #26421, .T. ) ;
#32977=ORIENTED_EDGE ( 'NONE', *, *, #13641, .T. ) ;
#32984=ORIENTED_EDGE ( 'NONE', *, *, #7869, .F. ) ;
#32999=DIRECTION ( 'NONE',  ( 0.000000000000000000, 0.000000000000000000, -1.000000000000000000 ) ) ;
#33006=EDGE_LOOP ( 'NONE', ( #24382, #13857, #3222, #29179 ) ) ;
#33008=DIRECTION ( 'NONE',  ( 0.000000000000000000, 0.000000000000000000, -1.000000000000000000 ) ) ;
#33019=ORIENTED_EDGE ( 'NONE', *, *, #7898, .F. ) ;
#33032=CIRCLE ( 'NONE', #44757, 9.999999999999998224 ) ;
#33036=ORIENTED_EDGE ( 'NONE', *, *, #42182, .T. ) ;
#33049=EDGE_LOOP ( 'NONE', ( #30884, #1725, #10511, #2503 ) ) ;
#33057=CARTESIAN_POINT ( 'NONE',  ( -30.36606260230379917, -53.11618894467930119, 11.84999999999999964 ) ) ;
#33068=ORIENTED_EDGE ( 'NONE', *, *, #31046, .F. ) ;
#33076=CARTESIAN_POINT ( 'NONE',  ( -15.33935108854907625, 24.23791302157028227, 10.84999999999999964 ) ) ;
#33094=ORIENTED_EDGE ( 'NONE', *, *, #45058, .F. ) ;
#33105=VERTEX_POINT ( 'NONE', #8788 ) ;
#33107=AXIS2_PLACEMENT_3D ( 'NONE', #18064, #14134, #10729 ) ;
#33116=CIRCLE ( 'NONE', #39025, 10.00000000000000888 ) ;
#33123=ORIENTED_EDGE ( 'NONE', *, *, #352, .F. ) ;
#33124=CONICAL_SURFACE ( 'NONE', #2180, 0.6299999999999998934, 0.7853981633974476129 ) ;
#33162=FACE_OUTER_BOUND ( 'NONE', #42175, .T. ) ;
#33165=EDGE_LOOP ( 'NONE', ( #22455, #17791, #1864, #13217 ) ) ;
#33175=ORIENTED_EDGE ( 'NONE', *, *, #28869, .T. ) ;
#33192=AXIS2_PLACEMENT_3D ( 'NONE', #23314, #15740, #35394 ) ;
#33196=LINE ( 'NONE', #25583, #46542 ) ;
#33199=VECTOR ( 'NONE', #41211, 999.9999999999998863 ) ;
#33207=CARTESIAN_POINT ( 'NONE',  ( 33.32492040275669609, -15.61618894397629909, 14.85000000026379396 ) ) ;
#33209=ORIENTED_EDGE ( 'NONE', *, *, #46636, .T. ) ;
#33221=CARTESIAN_POINT ( 'NONE',  ( 24.44780054039034667, -9.575813799495710654, -5.690000000000000391 ) ) ;
#33242=DIRECTION ( 'NONE',  ( 0.000000000000000000, 0.000000000000000000, 1.000000000000000000 ) ) ;
#33297=VECTOR ( 'NONE', #39960, 1000.000000000000000 ) ;
#33299=EDGE_LOOP ( 'NONE', ( #17710, #35550, #28647, #51245 ) ) ;
#33307=LINE ( 'NONE', #24907, #1583 ) ;
#33309=DIRECTION ( 'NONE',  ( -1.000000000000000000, 0.000000000000000000, 0.000000000000000000 ) ) ;
#33326=AXIS2_PLACEMENT_3D ( 'NONE', #16237, #39322, #47706 ) ;
#33328=VERTEX_POINT ( 'NONE', #16847 ) ;
#33335=DIRECTION ( 'NONE',  ( 0.000000000000000000, -1.000000000000000000, 0.000000000000000000 ) ) ;
#33344=DIRECTION ( 'NONE',  ( -1.224646799147353207E-16, 1.000000000000000000, 0.000000000000000000 ) ) ;
#33347=DIRECTION ( 'NONE',  ( -0.7071067811865475727, 0.7071067811865475727, 0.000000000000000000 ) ) ;
#33350=FACE_BOUND ( 'NONE', #40140, .T. ) ;
#33377=AXIS2_PLACEMENT_3D ( 'NONE', #45940, #10294, #37816 ) ;
#33390=VERTEX_POINT ( 'NONE', #19806 ) ;
#33415=CARTESIAN_POINT ( 'NONE',  ( 26.63393739736279997, -15.61618894439989980, -19.08999999982600215 ) ) ;
#33426=ORIENTED_EDGE ( 'NONE', *, *, #50559, .T. ) ;
#33429=DIRECTION ( 'NONE',  ( 0.000000000000000000, 0.000000000000000000, -1.000000000000000000 ) ) ;
#33434=CIRCLE ( 'NONE', #50298, 5.499999999999998224 ) ;
#33443=CARTESIAN_POINT ( 'NONE',  ( 16.13393739769620083, -15.61618894467929941, -2.149999999999999911 ) ) ;
#33459=EDGE_CURVE ( 'NONE', #434, #51110, #32419, .T. ) ;
#33471=AXIS2_PLACEMENT_3D ( 'NONE', #8812, #29226, #44969 ) ;
#33472=CARTESIAN_POINT ( 'NONE',  ( 16.13393739769620083, -15.61618894467929941, 17.35000000000000142 ) ) ;
#33500=VERTEX_POINT ( 'NONE', #12543 ) ;
#33514=AXIS2_PLACEMENT_3D ( 'NONE', #50653, #5857, #10309 ) ;
#33528=DIRECTION ( 'NONE',  ( 0.000000000000000000, 0.000000000000000000, -1.000000000000000000 ) ) ;
#33546=ADVANCED_BREP_SHAPE_REPRESENTATION ( '', ( #9246, #20940 ), #40219 ) ;
#33561=ORIENTED_EDGE ( 'NONE', *, *, #3135, .F. ) ;
#33565=CARTESIAN_POINT ( 'NONE',  ( -23.72016456855327249, -47.08947743092473814, 10.84999999999999964 ) ) ;
#33566=CARTESIAN_POINT ( 'NONE',  ( 16.13393739769620083, -15.61618894467929941, -16.88999999999999702 ) ) ;
#33570=DIRECTION ( 'NONE',  ( 1.000000000000000000, 0.000000000000000000, 0.000000000000000000 ) ) ;
#33575=EDGE_CURVE ( 'NONE', #51520, #6375, #41318, .T. ) ;
#33578=ADVANCED_FACE ( 'NONE', ( #20129 ), #31401, .F. ) ;
#33596=CARTESIAN_POINT ( 'NONE',  ( 22.23393739769620225, -15.61618894467929941, 14.34999999999999964 ) ) ;
#33598=ORIENTED_EDGE ( 'NONE', *, *, #48245, .F. ) ;
#33620=ORIENTED_EDGE ( 'NONE', *, *, #14592, .T. ) ;
#33627=CONICAL_SURFACE ( 'NONE', #51196, 0.6300000000000018918, 0.7853981633974476129 ) ;
#33630=AXIS2_PLACEMENT_3D ( 'NONE', #48919, #41293, #8557 ) ;
#33634=EDGE_CURVE ( 'NONE', #26465, #42921, #41278, .T. ) ;
#33635=CARTESIAN_POINT ( 'NONE',  ( 53.63393739769619373, -53.11618894467930119, 16.35000000000000142 ) ) ;
#33638=EDGE_CURVE ( 'NONE', #29187, #2702, #29561, .T. ) ;
#33639=ORIENTED_EDGE ( 'NONE', *, *, #30807, .F. ) ;
#33685=ORIENTED_EDGE ( 'NONE', *, *, #20720, .F. ) ;
#33688=DIRECTION ( 'NONE',  ( 0.000000000000000000, 0.000000000000000000, -1.000000000000000000 ) ) ;
#33713=CARTESIAN_POINT ( 'NONE',  ( 16.13393739769620083, -15.61618894467929941, 9.349999999999999645 ) ) ;
#33723=CIRCLE ( 'NONE', #21156, 20.00000000000000000 ) ;
#33742=ORIENTED_EDGE ( 'NONE', *, *, #27971, .T. ) ;
#33767=AXIS2_PLACEMENT_3D ( 'NONE', #37885, #2239, #37612 ) ;
#33837=DIRECTION ( 'NONE',  ( 0.000000000000000000, -0.7071067811865492381, -0.7071067811865457964 ) ) ;
#33868=CARTESIAN_POINT ( 'NONE',  ( 16.13393739769620083, -15.61618894467929941, 10.84999999999999964 ) ) ;
#33874=ORIENTED_EDGE ( 'NONE', *, *, #24191, .T. ) ;
#33878=ORIENTED_EDGE ( 'NONE', *, *, #20681, .T. ) ;
#33909=EDGE_CURVE ( 'NONE', #46283, #19834, #2795, .T. ) ;
#33922=DIRECTION ( 'NONE',  ( -1.062456999999999985E-16, 7.719205000000000365E-17, 1.000000000000000000 ) ) ;
#33934=ORIENTED_EDGE ( 'NONE', *, *, #4259, .T. ) ;
#33938=ORIENTED_EDGE ( 'NONE', *, *, #8321, .T. ) ;
#33942=DIRECTION ( 'NONE',  ( -0.5877852522924661427, -0.8090169943749525583, 0.000000000000000000 ) ) ;
#33963=DIRECTION ( 'NONE',  ( 0.000000000000000000, 1.000000000000000000, 0.000000000000000000 ) ) ;
#33976=VECTOR ( 'NONE', #17763, 1000.000000000000000 ) ;
#33981=CARTESIAN_POINT ( 'NONE',  ( 63.63393739769619373, -53.11618894467930119, 16.35000000000000142 ) ) ;
#33986=ORIENTED_EDGE ( 'NONE', *, *, #21041, .T. ) ;
#33993=DIRECTION ( 'NONE',  ( -1.000000000000000000, 0.000000000000000000, 0.000000000000000000 ) ) ;
#34011=ORIENTED_EDGE ( 'NONE', *, *, #5199, .T. ) ;
#34018=ORIENTED_EDGE ( 'NONE', *, *, #37281, .T. ) ;
#34052=AXIS2_PLACEMENT_3D ( 'NONE', #32395, #29005, #36604 ) ;
#34078=CARTESIAN_POINT ( 'NONE',  ( 33.20393739732724470, -15.61618894436410088, -14.68999999982327864 ) ) ;
#34091=CARTESIAN_POINT ( 'NONE',  ( -18.86606260230390220, 19.38381105532060289, 11.34999999999999964 ) ) ;
#34100=LINE ( 'NONE', #14208, #7120 ) ;
#34110=EDGE_CURVE ( 'NONE', #13022, #51110, #16176, .T. ) ;
#34114=DIRECTION ( 'NONE',  ( 1.000000000000000000, 0.000000000000000000, 0.000000000000000000 ) ) ;
#34185=DIRECTION ( 'NONE',  ( 0.000000000000000000, -1.000000000000000000, 0.000000000000000000 ) ) ;
#34188=AXIS2_PLACEMENT_3D ( 'NONE', #25995, #22062, #14474 ) ;
#34208=FACE_OUTER_BOUND ( 'NONE', #22913, .T. ) ;
#34215=ORIENTED_EDGE ( 'NONE', *, *, #27382, .F. ) ;
#34216=FILL_AREA_STYLE ('',( #22167 ) ) ;
#34218=CIRCLE ( 'NONE', #23329, 6.100000000000001421 ) ;
#34249=AXIS2_PLACEMENT_3D ( 'NONE', #31251, #23133, #50937 ) ;
#34275=CARTESIAN_POINT ( 'NONE',  ( 53.63393739769619373, -53.11618894467930119, 11.84999999999999964 ) ) ;
#34281=AXIS2_PLACEMENT_3D ( 'NONE', #49980, #49727, #6215 ) ;
#34284=AXIS2_PLACEMENT_3D ( 'NONE', #50215, #38414, #9609 ) ;
#34303=ORIENTED_EDGE ( 'NONE', *, *, #47000, .F. ) ;
#34329=ORIENTED_EDGE ( 'NONE', *, *, #37197, .F. ) ;
#34336=PLANE ( 'NONE',  #51853 ) ;
#34341=CIRCLE ( 'NONE', #36855, 5.999999999999998224 ) ;
#34355=CARTESIAN_POINT ( 'NONE',  ( 29.13393739769620083, -15.61618894467929941, -5.690000000000000391 ) ) ;
#34369=CIRCLE ( 'NONE', #11810, 5.500000000000000000 ) ;
#34387=DIRECTION ( 'NONE',  ( -0.7071067811865475727, 0.7071067811865475727, 0.000000000000000000 ) ) ;
#34392=ORIENTED_EDGE ( 'NONE', *, *, #43709, .F. ) ;
#34395=ORIENTED_EDGE ( 'NONE', *, *, #9053, .T. ) ;
#34398=DIRECTION ( 'NONE',  ( 0.000000000000000000, -1.000000000000000000, 0.000000000000000000 ) ) ;
#34443=VECTOR ( 'NONE', #22687, 1000.000000000000000 ) ;
#34455=LINE ( 'NONE', #50461, #5222 ) ;
#34457=VERTEX_POINT ( 'NONE', #25514 ) ;
#34477=FACE_OUTER_BOUND ( 'NONE', #50849, .T. ) ;
#34510=CARTESIAN_POINT ( 'NONE',  ( 51.13393739769659874, -50.61618894467899565, 11.34999999999999964 ) ) ;
#34515=EDGE_CURVE ( 'NONE', #17783, #24458, #44021, .T. ) ;
#34522=AXIS2_PLACEMENT_3D ( 'NONE', #39079, #35381, #2384 ) ;
#34571=DIRECTION ( 'NONE',  ( 0.000000000000000000, 0.000000000000000000, -1.000000000000000000 ) ) ;
#34577=ADVANCED_FACE ( 'NONE', ( #24068 ), #47216, .T. ) ;
#34592=CIRCLE ( 'NONE', #19525, 5.499999999999998224 ) ;
#34601=FACE_BOUND ( 'NONE', #17932, .T. ) ;
#34631=FACE_OUTER_BOUND ( 'NONE', #32705, .T. ) ;
#34651=CARTESIAN_POINT ( 'NONE',  ( 25.88393739769619728, -15.61618894467930119, -18.10000000000000142 ) ) ;
#34660=FACE_BOUND ( 'NONE', #30778, .T. ) ;
#34683=CIRCLE ( 'NONE', #49748, 28.27108544675919788 ) ;
#34697=EDGE_CURVE ( 'NONE', #16351, #44858, #46388, .T. ) ;
#34723=AXIS2_PLACEMENT_3D ( 'NONE', #28024, #20166, #4188 ) ;
#34724=EDGE_CURVE ( 'NONE', #29477, #28389, #37173, .T. ) ;
#34726=ORIENTED_EDGE ( 'NONE', *, *, #19790, .T. ) ;
#34732=CARTESIAN_POINT ( 'NONE',  ( 16.13393739769620083, -15.61618894467929941, 16.85000000000000142 ) ) ;
#34754=CARTESIAN_POINT ( 'NONE',  ( 3.133937397696200389, -15.61618894467929763, -5.690000000000000391 ) ) ;
#34764=CARTESIAN_POINT ( 'NONE',  ( 16.13393739767329649, -15.61618894439989980, -19.08999999984770213 ) ) ;
#34779=CIRCLE ( 'NONE', #11427, 10.27649999999999686 ) ;
#34787=EDGE_CURVE ( 'NONE', #49131, #26597, #40854, .T. ) ;
#34798=TOROIDAL_SURFACE ( 'NONE', #32268, 17.19098300429530113, 0.5000000000822009127 ) ;
#34814=CONICAL_SURFACE ( 'NONE', #12236, 0.6405000000000011795, 1.029744258676660307 ) ;
#34815=DIRECTION ( 'NONE',  ( -0.6934629132905123505, -0.5038302981000507552, 0.5150380749100490485 ) ) ;
#34821=CARTESIAN_POINT ( 'NONE',  ( 62.63393739769619373, -53.11618894467930119, 16.35000000000000142 ) ) ;
#34830=CARTESIAN_POINT ( 'NONE',  ( -31.36606260230380272, -53.11618894467930119, 16.35000000000000142 ) ) ;
#34869=EDGE_LOOP ( 'NONE', ( #42223, #3545, #7461, #13323, #27384 ) ) ;
#34913=VERTEX_POINT ( 'NONE', #43193 ) ;
#34922=ORIENTED_EDGE ( 'NONE', *, *, #48165, .T. ) ;
#34926=ORIENTED_EDGE ( 'NONE', *, *, #37343, .F. ) ;
#34941=ORIENTED_EDGE ( 'NONE', *, *, #14592, .F. ) ;
#34947=DIRECTION ( 'NONE',  ( -0.5877852522924764678, 0.8090169943749450088, 0.000000000000000000 ) ) ;
#34953=CYLINDRICAL_SURFACE ( 'NONE', #25872, 0.9999999999999988898 ) ;
#34956=DIRECTION ( 'NONE',  ( 1.000000000000000000, 0.000000000000000000, 0.000000000000000000 ) ) ;
#34976=CARTESIAN_POINT ( 'NONE',  ( -13.36606260230359844, -50.61618894467959962, 16.85000000000000142 ) ) ;
#34984=CARTESIAN_POINT ( 'NONE',  ( 16.13393739769620083, -15.61618894467929941, 17.07360679774999923 ) ) ;
#35021=FACE_OUTER_BOUND ( 'NONE', #3608, .T. ) ;
#35034=ORIENTED_EDGE ( 'NONE', *, *, #5385, .F. ) ;
#35049=CARTESIAN_POINT ( 'NONE',  ( 16.13393739769620083, -15.61618894467929941, 17.07360679774999923 ) ) ;
#35058=EDGE_CURVE ( 'NONE', #9595, #25307, #28774, .T. ) ;
#35063=ORIENTED_EDGE ( 'NONE', *, *, #46272, .F. ) ;
#35124=CIRCLE ( 'NONE', #43523, 4.649999999999999467 ) ;
#35146=DIRECTION ( 'NONE',  ( 0.000000000000000000, 1.000000000000000000, 0.000000000000000000 ) ) ;
#35147=ORIENTED_EDGE ( 'NONE', *, *, #5685, .F. ) ;
#35174=ADVANCED_FACE ( 'NONE', ( #5363 ), #17934, .T. ) ;
#35198=EDGE_CURVE ( 'NONE', #18843, #16350, #2719, .T. ) ;
#35201=AXIS2_PLACEMENT_3D ( 'NONE', #49186, #45504, #13281 ) ;
#35239=VERTEX_POINT ( 'NONE', #30477 ) ;
#35240=EDGE_LOOP ( 'NONE', ( #34392, #45082, #49578, #48590 ) ) ;
#35259=EDGE_CURVE ( 'NONE', #44094, #25374, #28809, .T. ) ;
#35277=FACE_OUTER_BOUND ( 'NONE', #1543, .T. ) ;
#35304=VERTEX_POINT ( 'NONE', #27324 ) ;
#35351=CYLINDRICAL_SURFACE ( 'NONE', #15654, 10.00000000000000711 ) ;
#35357=EDGE_CURVE ( 'NONE', #16668, #26662, #38870, .T. ) ;
#35368=EDGE_CURVE ( 'NONE', #44712, #40580, #34683, .T. ) ;
#35380=DIRECTION ( 'NONE',  ( -1.062456999999999985E-16, -7.719205000000000365E-17, -1.000000000000000000 ) ) ;
#35381=DIRECTION ( 'NONE',  ( -1.224646799147365533E-16, 1.000000000000000000, 8.684364315601308223E-16 ) ) ;
#35394=DIRECTION ( 'NONE',  ( -1.000000000000000000, 0.000000000000000000, 0.000000000000000000 ) ) ;
#35422=EDGE_CURVE ( 'NONE', #51387, #50052, #4536, .T. ) ;
#35429=ADVANCED_FACE ( 'NONE', ( #19722, #4252 ), #3753, .T. ) ;
#35454=CIRCLE ( 'NONE', #42155, 4.649999999999999467 ) ;
#35470=EDGE_LOOP ( 'NONE', ( #36985, #48905, #8819, #33598, #6745, #7788, #38978 ) ) ;
#35476=APPLICATION_CONTEXT ( 'automotive_design' ) ;
#35485=LINE ( 'NONE', #38913, #5679 ) ;
#35506=TOROIDAL_SURFACE ( 'NONE', #43884, 13.00000000000000000, 0.5000000000000000000 ) ;
#35510=CIRCLE ( 'NONE', #45532, 13.50000000000000178 ) ;
#35512=EDGE_LOOP ( 'NONE', ( #47700, #46537 ) ) ;
#35513=LINE ( 'NONE', #47326, #18226 ) ;
#35522=AXIS2_PLACEMENT_3D ( 'NONE', #43074, #38358, #18432 ) ;
#35526=DIRECTION ( 'NONE',  ( 1.000000000000000000, 0.000000000000000000, 0.000000000000000000 ) ) ;
#35530=ORIENTED_EDGE ( 'NONE', *, *, #9625, .F. ) ;
#35550=ORIENTED_EDGE ( 'NONE', *, *, #18802, .T. ) ;
#35555=CARTESIAN_POINT ( 'NONE',  ( -31.07316938349034885, 21.88381105532059934, 17.05710678118654755 ) ) ;
#35568=ORIENTED_EDGE ( 'NONE', *, *, #29319, .F. ) ;
#35574=VECTOR ( 'NONE', #31007, 1000.000000000000227 ) ;
#35579=VERTEX_POINT ( 'NONE', #25187 ) ;
#35588=CARTESIAN_POINT ( 'NONE',  ( 5.133937397696200833, -15.61618894467929763, -19.83999999999999986 ) ) ;
#35595=CIRCLE ( 'NONE', #38971, 0.9999999999999940048 ) ;
#35601=DIRECTION ( 'NONE',  ( 0.7071067811865475727, 0.7071067811865475727, 0.000000000000000000 ) ) ;
#35617=DIRECTION ( 'NONE',  ( 0.000000000000000000, 0.000000000000000000, 1.000000000000000000 ) ) ;
#35627=EDGE_CURVE ( 'NONE', #51462, #12691, #24601, .T. ) ;
#35628=ORIENTED_EDGE ( 'NONE', *, *, #25299, .F. ) ;
#35636=EDGE_LOOP ( 'NONE', ( #30007, #22650, #14982, #26332, #24069, #21022 ) ) ;
#35664=PRODUCT ( 'Top Mounting Plate', 'Top Mounting Plate', '', ( #16245 ) ) ;
#35667=AXIS2_PLACEMENT_3D ( 'NONE', #27471, #19358, #7579 ) ;
#35687=DIRECTION ( 'NONE',  ( 1.000000000000000000, 0.000000000000000000, 0.000000000000000000 ) ) ;
#35709=DIRECTION ( 'NONE',  ( 0.000000000000000000, 0.000000000000000000, 1.000000000000000000 ) ) ;
#35721=ADVANCED_FACE ( 'NONE', ( #47207 ), #2136, .T. ) ;
#35781=DIRECTION ( 'NONE',  ( -2.840828347717470042E-11, 6.470619327693540153E-12, 1.000000000000000000 ) ) ;
#35818=CARTESIAN_POINT ( 'NONE',  ( 53.63393739769619373, -53.11618894467930119, 17.35000000000000142 ) ) ;
#35831=EDGE_CURVE ( 'NONE', #49915, #46911, #13795, .T. ) ;
#35834=PLANE ( 'NONE',  #1654 ) ;
#35843=AXIS2_PLACEMENT_3D ( 'NONE', #47637, #51315, #48147 ) ;
#35847=VERTEX_POINT ( 'NONE', #27777 ) ;
#35858=DIRECTION ( 'NONE',  ( -1.000000000000000000, 0.000000000000000000, 0.000000000000000000 ) ) ;
#35915=CIRCLE ( 'NONE', #51000, 5.499999999999998224 ) ;
#35932=ORIENTED_EDGE ( 'NONE', *, *, #50164, .F. ) ;
#35933=FACE_OUTER_BOUND ( 'NONE', #18355, .T. ) ;
#35944=ORIENTED_EDGE ( 'NONE', *, *, #3477, .T. ) ;
#35952=VECTOR ( 'NONE', #33570, 1000.000000000000000 ) ;
#35955=AXIS2_PLACEMENT_3D ( 'NONE', #28811, #28287, #4201 ) ;
#35959=AXIS2_PLACEMENT_3D ( 'NONE', #45939, #33344, #10028 ) ;
#35979=VECTOR ( 'NONE', #36329, 1000.000000000000000 ) ;
#35981=AXIS2_PLACEMENT_3D ( 'NONE', #43455, #11232, #31372 ) ;
#35997=FACE_OUTER_BOUND ( 'NONE', #27238, .T. ) ;
#36010=EDGE_CURVE ( 'NONE', #18473, #11039, #48964, .T. ) ;
#36015=LINE ( 'NONE', #895, #33297 ) ;
#36024=TOROIDAL_SURFACE ( 'NONE', #35201, 18.00000000000000000, 2.000000000000000000 ) ;
#36027=CLOSED_SHELL ( 'NONE', ( #43194, #7321, #21526, #16065, #46675, #34577, #44231, #13921, #1699, #42612, #13427, #41454, #39890, #39865, #47472, #37029, #2082, #19804, #10806, #29896, #28299, #4242, #9346, #31566, #24980, #13048, #27560, #42415, #21280, #5781, #46294, #4198, #26669, #3488, #11617, #28016, #50983, #16970, #39570, #4612, #4721, #31209, #32139, #47050, #37426, #40289, #8451, #35429, #42550, #8197, #11233, #44825, #14184, #38459, #35174, #32391, #48505, #29094, #25424, #24915, #9105, #10933, #14917, #13099, #49819, #13598, #23699, #37069, #29075, #27080, #29209, #2886, #42374, #11851, #27728, #40629, #33578, #20512, #40261, #25854, #13986, #35721, #32507, #39390, #21169, #18439, #43718, #31686, #1531, #6965, #5137, #4966, #29006, #42162, #47629, #17408, #21376, #24572, #28665, #41584, #12245, #15363, #48680, #26143, #31373, #14055, #4180, #45128, #9058, #49168, #25568, #44608, #24343, #18934, #8575, #7763, #512 ) ) ;
#36036=( NAMED_UNIT ( * ) PLANE_ANGLE_UNIT ( ) SI_UNIT ( $, .RADIAN. ) );
#36041=CARTESIAN_POINT ( 'NONE',  ( 54.66064891145146731, -55.47029091092863240, 17.35000000000000142 ) ) ;
#36060=DIRECTION ( 'NONE',  ( -9.408764999999898798E-18, 1.274833000000000002E-16, 1.000000000000000000 ) ) ;
#36067=ORIENTED_EDGE ( 'NONE', *, *, #22207, .T. ) ;
#36077=EDGE_CURVE ( 'NONE', #16351, #23557, #28801, .T. ) ;
#36121=CARTESIAN_POINT ( 'NONE',  ( -21.36606260230379917, 31.59091783650714547, 17.05710678118654755 ) ) ;
#36133=CARTESIAN_POINT ( 'NONE',  ( 17.00689302767908728, -16.25042833492357985, -9.392532499999980189 ) ) ;
#36156=CARTESIAN_POINT ( 'NONE',  ( 51.13393739769659874, -50.61618894467899565, 14.21249999999999858 ) ) ;
#36160=DIRECTION ( 'NONE',  ( -1.000000000000000000, 0.000000000000000000, 0.000000000000000000 ) ) ;
#36196=EDGE_CURVE ( 'NONE', #19506, #16944, #15480, .T. ) ;
#36200=CARTESIAN_POINT ( 'NONE',  ( -1.057045605833899948, -15.61618894397629731, 14.85000000069720549 ) ) ;
#36202=ORIENTED_EDGE ( 'NONE', *, *, #38745, .F. ) ;
#36251=ORIENTED_EDGE ( 'NONE', *, *, #14626, .F. ) ;
#36257=EDGE_CURVE ( 'NONE', #35579, #8558, #33032, .T. ) ;
#36263=CARTESIAN_POINT ( 'NONE',  ( -14.01196063605389774, -47.08947743092479499, 17.35000000000000142 ) ) ;
#36275=DIRECTION ( 'NONE',  ( 0.000000000000000000, 0.000000000000000000, -1.000000000000000000 ) ) ;
#36277=DIRECTION ( 'NONE',  ( 0.000000000000000000, -1.000000000000000000, 0.000000000000000000 ) ) ;
#36310=DIRECTION ( 'NONE',  ( 0.000000000000000000, 0.000000000000000000, 1.000000000000000000 ) ) ;
#36329=DIRECTION ( 'NONE',  ( 0.000000000000000000, 0.000000000000000000, -1.000000000000000000 ) ) ;
#36340=DIRECTION ( 'NONE',  ( 0.000000000000000000, 0.000000000000000000, 1.000000000000000000 ) ) ;
#36349=EDGE_CURVE ( 'NONE', #25361, #42283, #22146, .T. ) ;
#36357=EDGE_CURVE ( 'NONE', #6962, #434, #44998, .T. ) ;
#36377=( GEOMETRIC_REPRESENTATION_CONTEXT ( 3 ) GLOBAL_UNCERTAINTY_ASSIGNED_CONTEXT ( ( #30032 ) ) GLOBAL_UNIT_ASSIGNED_CONTEXT ( ( #38433, #36036, #31318 ) ) REPRESENTATION_CONTEXT ( 'NONE', 'WORKASPACE' ) );
#36395=DIRECTION ( 'NONE',  ( 0.000000000000000000, 0.000000000000000000, -1.000000000000000000 ) ) ;
#36413=DIRECTION ( 'NONE',  ( 1.000000000000000000, 0.000000000000000000, 0.000000000000000000 ) ) ;
#36420=DIRECTION ( 'NONE',  ( -1.000000000000000000, 0.000000000000000000, 0.000000000000000000 ) ) ;
#36468=EDGE_CURVE ( 'NONE', #18307, #44616, #47289, .T. ) ;
#36477=CARTESIAN_POINT ( 'NONE',  ( 10.03393739769619941, -15.61618894467929941, 2.750000000000000000 ) ) ;
#36487=DIRECTION ( 'NONE',  ( -1.000000000000000000, 0.000000000000000000, 0.000000000000000000 ) ) ;
#36497=DIRECTION ( 'NONE',  ( 0.000000000000000000, 0.000000000000000000, -1.000000000000000000 ) ) ;
#36524=ORIENTED_EDGE ( 'NONE', *, *, #22738, .F. ) ;
#36536=LINE ( 'NONE', #47837, #824 ) ;
#36556=DIRECTION ( 'NONE',  ( 1.000000000000000000, 0.000000000000000000, 0.000000000000000000 ) ) ;
#36578=ORIENTED_EDGE ( 'NONE', *, *, #14670, .T. ) ;
#36589=CYLINDRICAL_SURFACE ( 'NONE', #11946, 13.50000000000000178 ) ;
#36604=DIRECTION ( 'NONE',  ( -1.000000000000000000, 0.000000000000000000, 0.000000000000000000 ) ) ;
#36628=DIRECTION ( 'NONE',  ( 0.000000000000000000, 0.000000000000000000, 1.000000000000000000 ) ) ;
#36642=EDGE_LOOP ( 'NONE', ( #23309, #51067, #37488, #9157 ) ) ;
#36676=DIRECTION ( 'NONE',  ( -1.000000000000000000, 0.000000000000000000, 0.000000000000000000 ) ) ;
#36678=DIRECTION ( 'NONE',  ( 0.000000000000000000, 0.000000000000000000, 1.000000000000000000 ) ) ;
#36733=DIRECTION ( 'NONE',  ( 0.000000000000000000, 0.000000000000000000, 1.000000000000000000 ) ) ;
#36737=CARTESIAN_POINT ( 'NONE',  ( 16.13393739769620083, -15.61618894467929941, -8.849999999999999645 ) ) ;
#36746=DIRECTION ( 'NONE',  ( 0.000000000000000000, 0.000000000000000000, -1.000000000000000000 ) ) ;
#36747=ORIENTED_EDGE ( 'NONE', *, *, #25145, .T. ) ;
#36763=EDGE_CURVE ( 'NONE', #15443, #17150, #26362, .T. ) ;
#36771=VECTOR ( 'NONE', #4282, 1000.000000000000000 ) ;
#36776=ORIENTED_EDGE ( 'NONE', *, *, #42948, .F. ) ;
#36778=VECTOR ( 'NONE', #21234, 1000.000000000000000 ) ;
#36781=PLANE ( 'NONE',  #19344 ) ;
#36783=CARTESIAN_POINT ( 'NONE',  ( 2.633937397696199945, -15.61618894467929763, -6.189999999999999503 ) ) ;
#36796=DIRECTION ( 'NONE',  ( 0.000000000000000000, 0.000000000000000000, 1.000000000000000000 ) ) ;
#36803=CIRCLE ( 'NONE', #20899, 5.500000000000000000 ) ;
#36826=LINE ( 'NONE', #929, #15423 ) ;
#36848=AXIS2_PLACEMENT_3D ( 'NONE', #40035, #36340, #40802 ) ;
#36854=TOROIDAL_SURFACE ( 'NONE', #32637, 25.00000000000000000, 3.569999999999939888 ) ;
#36855=AXIS2_PLACEMENT_3D ( 'NONE', #12433, #13231, #631 ) ;
#36860=CARTESIAN_POINT ( 'NONE',  ( 16.13393739769620083, -15.61618894467929941, -8.655000000000001137 ) ) ;
#36884=CARTESIAN_POINT ( 'NONE',  ( 30.63393739769619728, -15.61618894467929941, -20.58999999999999986 ) ) ;
#36891=CARTESIAN_POINT ( 'NONE',  ( 16.13393739769620083, -15.61618894467929941, -1.149999999999999911 ) ) ;
#36908=ORIENTED_EDGE ( 'NONE', *, *, #7339, .T. ) ;
#36915=EDGE_LOOP ( 'NONE', ( #30307, #26073, #20074, #47318 ) ) ;
#36918=CARTESIAN_POINT ( 'NONE',  ( 51.13393739769620083, 19.38381105532069881, 11.34999999999999964 ) ) ;
#36950=CARTESIAN_POINT ( 'NONE',  ( -18.86606260230390220, 19.38381105532060289, 11.97999999999999865 ) ) ;
#36957=AXIS2_PLACEMENT_3D ( 'NONE', #5760, #28816, #45341 ) ;
#36960=AXIS2_PLACEMENT_3D ( 'NONE', #5106, #20799, #8244 ) ;
#36980=DIRECTION ( 'NONE',  ( 0.000000000000000000, -1.000000000000000000, 0.000000000000000000 ) ) ;
#36984=ORIENTED_EDGE ( 'NONE', *, *, #11590, .T. ) ;
#36985=ORIENTED_EDGE ( 'NONE', *, *, #6820, .T. ) ;
#37029=ADVANCED_FACE ( 'NONE', ( #44545 ), #18869, .T. ) ;
#37031=DIRECTION ( 'NONE',  ( -0.8090169943749466741, -0.5877852522924741363, 0.000000000000000000 ) ) ;
#37032=LINE ( 'NONE', #12939, #38331 ) ;
#37039=CARTESIAN_POINT ( 'NONE',  ( 34.63393739890910439, -15.61618894518879941, 4.349999999448538546 ) ) ;
#37041=VECTOR ( 'NONE', #6068, 1000.000000000000000 ) ;
#37044=ORIENTED_EDGE ( 'NONE', *, *, #12964, .T. ) ;
#37069=ADVANCED_FACE ( 'NONE', ( #23828 ), #31380, .F. ) ;
#37070=EDGE_CURVE ( 'NONE', #26662, #16668, #8816, .T. ) ;
#37074=VECTOR ( 'NONE', #37537, 1000.000000000000000 ) ;
#37110=ORIENTED_EDGE ( 'NONE', *, *, #29368, .F. ) ;
#37112=AXIS2_PLACEMENT_3D ( 'NONE', #37039, #24955, #3333 ) ;
#37128=DIRECTION ( 'NONE',  ( 0.7071067811865475727, -0.7071067811865475727, 0.000000000000000000 ) ) ;
#37132=EDGE_CURVE ( 'NONE', #26710, #13022, #32231, .T. ) ;
#37159=APPLICATION_CONTEXT ( 'automotive_design' ) ;
#37173=CIRCLE ( 'NONE', #45519, 5.500000000000000000 ) ;
#37178=DIRECTION ( 'NONE',  ( 0.000000000000000000, 0.000000000000000000, -1.000000000000000000 ) ) ;
#37193=ORIENTED_EDGE ( 'NONE', *, *, #16308, .F. ) ;
#37197=EDGE_CURVE ( 'NONE', #25307, #33390, #5752, .T. ) ;
#37210=EDGE_CURVE ( 'NONE', #47819, #8620, #35595, .T. ) ;
#37215=DIRECTION ( 'NONE',  ( 0.000000000000000000, -1.000000000000000000, 0.000000000000000000 ) ) ;
#37219=AXIS2_PLACEMENT_3D ( 'NONE', #3317, #30813, #18775 ) ;
#37223=CIRCLE ( 'NONE', #7821, 5.499999999999998224 ) ;
#37240=CARTESIAN_POINT ( 'NONE',  ( -1.504259202252973493, -15.61618894397937751, 14.62639320225000006 ) ) ;
#37243=DIRECTION ( 'NONE',  ( 0.000000000000000000, -1.000000000000000000, 0.000000000000000000 ) ) ;
#37244=DIRECTION ( 'NONE',  ( 0.000000000000000000, 0.000000000000000000, -1.000000000000000000 ) ) ;
#37255=DIRECTION ( 'NONE',  ( 1.224646799147353207E-16, 1.000000000000000000, -0.000000000000000000 ) ) ;
#37273=AXIS2_PLACEMENT_3D ( 'NONE', #50878, #7371, #15745 ) ;
#37281=EDGE_CURVE ( 'NONE', #33328, #16351, #40622, .T. ) ;
#37282=CARTESIAN_POINT ( 'NONE',  ( -21.36606260230379917, 21.88381105532059934, 17.35000000000000142 ) ) ;
#37293=AXIS2_PLACEMENT_3D ( 'NONE', #10656, #50740, #35526 ) ;
#37303=AXIS2_PLACEMENT_3D ( 'NONE', #16470, #49239, #24308 ) ;
#37316=DIRECTION ( 'NONE',  ( -1.000000000000000000, 0.000000000000000000, 0.000000000000000000 ) ) ;
#37335=EDGE_CURVE ( 'NONE', #27635, #2118, #45707, .T. ) ;
#37343=EDGE_CURVE ( 'NONE', #35847, #31353, #42964, .T. ) ;
#37362=EDGE_CURVE ( 'NONE', #1900, #8620, #23011, .T. ) ;
#37375=ORIENTED_EDGE ( 'NONE', *, *, #36349, .F. ) ;
#37379=DIRECTION ( 'NONE',  ( 0.000000000000000000, 0.000000000000000000, 1.000000000000000000 ) ) ;
#37414=ORIENTED_EDGE ( 'NONE', *, *, #35627, .F. ) ;
#37426=ADVANCED_FACE ( 'NONE', ( #49789 ), #34798, .F. ) ;
#37488=ORIENTED_EDGE ( 'NONE', *, *, #836, .T. ) ;
#37510=EDGE_LOOP ( 'NONE', ( #28588, #4106, #32676, #12900 ) ) ;
#37537=DIRECTION ( 'NONE',  ( 0.000000000000000000, 0.000000000000000000, 1.000000000000000000 ) ) ;
#37541=CARTESIAN_POINT ( 'NONE',  ( 21.06894106338335604, -12.03069890569523714, -8.849999999999999645 ) ) ;
#37558=ORIENTED_EDGE ( 'NONE', *, *, #19416, .T. ) ;
#37567=ORIENTED_EDGE ( 'NONE', *, *, #7339, .F. ) ;
#37590=CIRCLE ( 'NONE', #24174, 3.569999999999939444 ) ;
#37595=CARTESIAN_POINT ( 'NONE',  ( -30.36606260230379917, 21.88381105532059934, 10.84999999999999964 ) ) ;
#37612=DIRECTION ( 'NONE',  ( -1.000000000000000000, 0.000000000000000000, 0.000000000000000000 ) ) ;
#37619=ORIENTED_EDGE ( 'NONE', *, *, #51008, .F. ) ;
#37633=EDGE_CURVE ( 'NONE', #44858, #32800, #7175, .T. ) ;
#37640=VECTOR ( 'NONE', #26751, 1000.000000000000114 ) ;
#37642=AXIS2_PLACEMENT_3D ( 'NONE', #46267, #29723, #5897 ) ;
#37653=ORIENTED_EDGE ( 'NONE', *, *, #32368, .F. ) ;
#37658=CARTESIAN_POINT ( 'NONE',  ( 39.88393739769619373, 30.88381105532059934, 16.35000000000000142 ) ) ;
#37665=ORIENTED_EDGE ( 'NONE', *, *, #37878, .T. ) ;
#37690=FACE_OUTER_BOUND ( 'NONE', #24194, .T. ) ;
#37694=CARTESIAN_POINT ( 'NONE',  ( 16.13393739769620083, -15.61618894467929941, -5.966499999999999915 ) ) ;
#37722=CIRCLE ( 'NONE', #44417, 0.5000000000000000000 ) ;
#37728=CARTESIAN_POINT ( 'NONE',  ( 33.32492040332130045, -15.61618894398128177, 14.34999999999999964 ) ) ;
#37764=AXIS2_PLACEMENT_3D ( 'NONE', #29627, #46681, #30140 ) ;
#37772=CARTESIAN_POINT ( 'NONE',  ( -2.366062599821302292, -15.61618894518879763, 4.350000001194220367 ) ) ;
#37789=EDGE_CURVE ( 'NONE', #23557, #47819, #13865, .T. ) ;
#37793=CIRCLE ( 'NONE', #47021, 1.000000000000000888 ) ;
#37796=AXIS2_PLACEMENT_3D ( 'NONE', #4532, #36497, #12676 ) ;
#37805=ORIENTED_EDGE ( 'NONE', *, *, #22992, .T. ) ;
#37816=DIRECTION ( 'NONE',  ( 1.000000000000000000, 0.000000000000000000, 0.000000000000000000 ) ) ;
#37867=AXIS2_PLACEMENT_3D ( 'NONE', #50410, #17399, #41758 ) ;
#37878=EDGE_CURVE ( 'NONE', #48268, #9595, #21398, .T. ) ;
#37885=CARTESIAN_POINT ( 'NONE',  ( 51.13393739769620083, 19.38381105532069881, 16.85000000000000142 ) ) ;
#37892=ORIENTED_EDGE ( 'NONE', *, *, #13735, .T. ) ;
#37900=DIRECTION ( 'NONE',  ( -1.000000000000000000, 0.000000000000000000, 0.000000000000000000 ) ) ;
#37922=DIRECTION ( 'NONE',  ( -0.8090169943749453418, 0.5877852522924759127, 0.000000000000000000 ) ) ;
#37923=DIRECTION ( 'NONE',  ( 0.000000000000000000, 0.000000000000000000, -1.000000000000000000 ) ) ;
#37932=ORIENTED_EDGE ( 'NONE', *, *, #27466, .T. ) ;
#37947=FACE_OUTER_BOUND ( 'NONE', #3941, .T. ) ;
#37990=CARTESIAN_POINT ( 'NONE',  ( 29.63393739769619728, -15.61618894467929941, -2.149999999999999911 ) ) ;
#37995=CARTESIAN_POINT ( 'NONE',  ( 7.820074255002050556, -9.575813799495708878, -18.58999999999999986 ) ) ;
#38041=DIRECTION ( 'NONE',  ( 0.000000000000000000, -1.000000000000000000, 0.000000000000000000 ) ) ;
#38050=VECTOR ( 'NONE', #7130, 1000.000000000000114 ) ;
#38118=ORIENTED_EDGE ( 'NONE', *, *, #26717, .F. ) ;
#38132=CARTESIAN_POINT ( 'NONE',  ( -18.86606260230390220, 13.88381105532060289, 16.85000000000000142 ) ) ;
#38146=ORIENTED_EDGE ( 'NONE', *, *, #14710, .F. ) ;
#38179=SURFACE_STYLE_FILL_AREA ( #34216 ) ;
#38181=DIRECTION ( 'NONE',  ( 0.000000000000000000, 0.000000000000000000, -1.000000000000000000 ) ) ;
#38216=FACE_OUTER_BOUND ( 'NONE', #38767, .T. ) ;
#38231=AXIS2_PLACEMENT_3D ( 'NONE', #30241, #46262, #10348 ) ;
#38255=EDGE_LOOP ( 'NONE', ( #19782, #38531, #47169, #9549, #2617, #50799, #5291 ) ) ;
#38258=LINE ( 'NONE', #26968, #12807 ) ;
#38311=VERTEX_POINT ( 'NONE', #36783 ) ;
#38319=EDGE_LOOP ( 'NONE', ( #13164, #7017, #49274, #50108 ) ) ;
#38328=FACE_OUTER_BOUND ( 'NONE', #24137, .T. ) ;
#38331=VECTOR ( 'NONE', #29156, 1000.000000000000000 ) ;
#38358=DIRECTION ( 'NONE',  ( 0.000000000000000000, 0.000000000000000000, -1.000000000000000000 ) ) ;
#38366=TOROIDAL_SURFACE ( 'NONE', #19932, 10.49999999968949815, 0.4999999999856510335 ) ;
#38373=ORIENTED_EDGE ( 'NONE', *, *, #30807, .T. ) ;
#38414=DIRECTION ( 'NONE',  ( 0.000000000000000000, 0.000000000000000000, -1.000000000000000000 ) ) ;
#38433=( LENGTH_UNIT ( ) NAMED_UNIT ( * ) SI_UNIT ( .MILLI., .METRE. ) );
#38459=ADVANCED_FACE ( 'NONE', ( #18940 ), #495, .T. ) ;
#38461=LINE ( 'NONE', #22714, #33976 ) ;
#38531=ORIENTED_EDGE ( 'NONE', *, *, #37210, .T. ) ;
#38553=ORIENTED_EDGE ( 'NONE', *, *, #12009, .F. ) ;
#38594=VECTOR ( 'NONE', #44025, 1000.000000000000000 ) ;
#38598=PLANE ( 'NONE',  #33377 ) ;
#38618=CYLINDRICAL_SURFACE ( 'NONE', #37867, 10.00000000000000711 ) ;
#38634=CIRCLE ( 'NONE', #1760, 9.999999999999998224 ) ;
#38645=ORIENTED_EDGE ( 'NONE', *, *, #8917, .T. ) ;
#38650=CARTESIAN_POINT ( 'NONE',  ( 51.13393739769659874, -50.61618894467899565, 11.97999999999999865 ) ) ;
#38658=CARTESIAN_POINT ( 'NONE',  ( -2.366062601062550730, -15.61618894523020629, 9.350000000582056714 ) ) ;
#38681=DIRECTION ( 'NONE',  ( 1.000000000000000000, 0.000000000000000000, 0.000000000000000000 ) ) ;
#38687=ORIENTED_EDGE ( 'NONE', *, *, #44093, .T. ) ;
#38727=CARTESIAN_POINT ( 'NONE',  ( 16.13393739769620083, -15.61618894467929941, -14.88746750000000141 ) ) ;
#38745=EDGE_CURVE ( 'NONE', #26084, #6962, #12255, .T. ) ;
#38751=EDGE_LOOP ( 'NONE', ( #44106, #32220, #49904, #6569 ) ) ;
#38767=EDGE_LOOP ( 'NONE', ( #43857, #23447, #31863, #27505, #4815 ) ) ;
#38789=DIRECTION ( 'NONE',  ( -0.8090169943749462300, -0.5877852522924749135, 0.000000000000000000 ) ) ;
#38807=ORIENTED_EDGE ( 'NONE', *, *, #45351, .F. ) ;
#38816=AXIS2_PLACEMENT_3D ( 'NONE', #26582, #49430, #42598 ) ;
#38820=CARTESIAN_POINT ( 'NONE',  ( 53.63393739769619373, -62.11618894467930119, 10.84999999999999964 ) ) ;
#38832=EDGE_CURVE ( 'NONE', #41343, #26710, #21929, .T. ) ;
#38870=CIRCLE ( 'NONE', #35522, 17.19098300562509962 ) ;
#38912=DIRECTION ( 'NONE',  ( 0.000000000000000000, 0.000000000000000000, -1.000000000000000000 ) ) ;
#38913=CARTESIAN_POINT ( 'NONE',  ( 2.633937397696199945, -15.61618894467929763, -8.655000000000001137 ) ) ;
#38943=VECTOR ( 'NONE', #36676, 1000.000000000000000 ) ;
#38959=ORIENTED_EDGE ( 'NONE', *, *, #37362, .F. ) ;
#38971=AXIS2_PLACEMENT_3D ( 'NONE', #21970, #49016, #12852 ) ;
#38978=ORIENTED_EDGE ( 'NONE', *, *, #38745, .T. ) ;
#38993=DIRECTION ( 'NONE',  ( 1.000000000000000000, 0.000000000000000000, 0.000000000000000000 ) ) ;
#39017=CARTESIAN_POINT ( 'NONE',  ( -3.366062602303800055, -15.61618894467929763, -15.18999999999999950 ) ) ;
#39025=AXIS2_PLACEMENT_3D ( 'NONE', #23198, #15627, #51272 ) ;
#39056=ORIENTED_EDGE ( 'NONE', *, *, #38832, .T. ) ;
#39062=DIRECTION ( 'NONE',  ( 1.000000000000000000, 0.000000000000000000, 0.000000000000000000 ) ) ;
#39079=CARTESIAN_POINT ( 'NONE',  ( 41.13393739769610136, -15.61618894467929586, 7.920000000000036344 ) ) ;
#39091=CYLINDRICAL_SURFACE ( 'NONE', #21718, 9.999999999999998224 ) ;
#39126=VERTEX_POINT ( 'NONE', #21102 ) ;
#39131=EDGE_LOOP ( 'NONE', ( #32945, #5123, #5188, #49424 ) ) ;
#39144=DIRECTION ( 'NONE',  ( -1.000000000000000000, 0.000000000000000000, 0.000000000000000000 ) ) ;
#39157=AXIS2_PLACEMENT_3D ( 'NONE', #3534, #51233, #19505 ) ;
#39185=EDGE_CURVE ( 'NONE', #42670, #6855, #1404, .T. ) ;
#39200=DIRECTION ( 'NONE',  ( 1.000000000000000000, 0.000000000000000000, 0.000000000000000000 ) ) ;
#39208=EDGE_CURVE ( 'NONE', #6375, #12691, #11440, .T. ) ;
#39260=DIRECTION ( 'NONE',  ( -1.000000000000000000, 0.000000000000000000, 0.000000000000000000 ) ) ;
#39262=AXIS2_PLACEMENT_3D ( 'NONE', #37772, #42220, #26469 ) ;
#39265=DIRECTION ( 'NONE',  ( -1.000000000000000000, 0.000000000000000000, 0.000000000000000000 ) ) ;
#39268=CARTESIAN_POINT ( 'NONE',  ( 45.63393739769620083, 19.38381105532069881, 16.85000000000000142 ) ) ;
#39280=EDGE_CURVE ( 'NONE', #10844, #32800, #30679, .T. ) ;
#39283=CARTESIAN_POINT ( 'NONE',  ( 27.13393739769620083, -15.61618894467929941, -19.83999999999999986 ) ) ;
#39321=EDGE_LOOP ( 'NONE', ( #27892, #7929 ) ) ;
#39322=DIRECTION ( 'NONE',  ( 0.000000000000000000, 0.000000000000000000, -1.000000000000000000 ) ) ;
#39383=ORIENTED_EDGE ( 'NONE', *, *, #32241, .T. ) ;
#39390=ADVANCED_FACE ( 'NONE', ( #29899 ), #1887, .T. ) ;
#39394=CARTESIAN_POINT ( 'NONE',  ( 50.62425669123998517, 19.01350634637644532, 11.97999999999999865 ) ) ;
#39412=ORIENTED_EDGE ( 'NONE', *, *, #35368, .F. ) ;
#39416=DIRECTION ( 'NONE',  ( -1.000000000000000000, 0.000000000000000000, 0.000000000000000000 ) ) ;
#39448=CIRCLE ( 'NONE', #18518, 1.000000000000000888 ) ;
#39482=CARTESIAN_POINT ( 'NONE',  ( 53.63393739769619373, 21.88381105532059934, 11.84999999999999964 ) ) ;
#39491=CARTESIAN_POINT ( 'NONE',  ( 62.63393739769619373, 21.88381105532059934, 17.35000000000000142 ) ) ;
#39505=DIRECTION ( 'NONE',  ( 1.000000000000000000, 0.000000000000000000, 0.000000000000000000 ) ) ;
#39516=CIRCLE ( 'NONE', #18587, 5.499999999999998224 ) ;
#39518=DIRECTION ( 'NONE',  ( -2.066387465239710029E-12, 1.205421602240320019E-11, 1.000000000000000000 ) ) ;
#39526=CARTESIAN_POINT ( 'NONE',  ( -21.36606260230379917, -62.11618894467930119, 11.84999999999999964 ) ) ;
#39535=EDGE_CURVE ( 'NONE', #19506, #19682, #48282, .T. ) ;
#39558=VERTEX_POINT ( 'NONE', #31697 ) ;
#39570=ADVANCED_FACE ( 'NONE', ( #43282 ), #46506, .F. ) ;
#39587=ORIENTED_EDGE ( 'NONE', *, *, #44093, .F. ) ;
#39592=CARTESIAN_POINT ( 'NONE',  ( 53.63393739769619373, 21.88381105532059934, 16.35000000000000142 ) ) ;
#39595=CARTESIAN_POINT ( 'NONE',  ( -19.23636731124815924, 19.89349176177682210, 11.97999999999999865 ) ) ;
#39601=CIRCLE ( 'NONE', #245, 17.63819660112499932 ) ;
#39607=DIRECTION ( 'NONE',  ( 0.000000000000000000, 0.000000000000000000, -1.000000000000000000 ) ) ;
#39613=CARTESIAN_POINT ( 'NONE',  ( 16.13393739769620083, -15.61618894467929941, -8.655000000000001137 ) ) ;
#39623=CONICAL_SURFACE ( 'NONE', #23694, 0.6299999999999998934, 0.7853981633974476129 ) ;
#39642=CARTESIAN_POINT ( 'NONE',  ( 51.13393739769659874, -50.61618894467899565, 11.34999999999999964 ) ) ;
#39647=VECTOR ( 'NONE', #36628, 1000.000000000000000 ) ;
#39658=AXIS2_PLACEMENT_3D ( 'NONE', #34275, #3372, #19082 ) ;
#39660=DIRECTION ( 'NONE',  ( 0.000000000000000000, -1.000000000000000000, 0.000000000000000000 ) ) ;
#39698=CIRCLE ( 'NONE', #25449, 36.50000000000000711 ) ;
#39708=DIRECTION ( 'NONE',  ( 0.000000000000000000, 0.000000000000000000, -1.000000000000000000 ) ) ;
#39709=ORIENTED_EDGE ( 'NONE', *, *, #45978, .F. ) ;
#39710=ORIENTED_EDGE ( 'NONE', *, *, #30493, .F. ) ;
#39723=TOROIDAL_SURFACE ( 'NONE', #32173, 9.000000000000000000, 1.000000000000000000 ) ;
#39734=CARTESIAN_POINT ( 'NONE',  ( 55.58353086675839450, 22.61662994292931117, 16.85000000000000142 ) ) ;
#39746=CARTESIAN_POINT ( 'NONE',  ( 2.633937397696199945, -15.61618894435254745, -11.11999999999999922 ) ) ;
#39749=CARTESIAN_POINT ( 'NONE',  ( 16.13393739769620083, -15.61618894467929941, -19.08999999999999986 ) ) ;
#39798=CARTESIAN_POINT ( 'NONE',  ( 16.13393739769620083, -15.61618894467929941, -6.189999999999999503 ) ) ;
#39805=DIRECTION ( 'NONE',  ( 1.000000000000000000, 0.000000000000000000, 0.000000000000000000 ) ) ;
#39865=ADVANCED_FACE ( 'NONE', ( #29078 ), #13054, .T. ) ;
#39870=DIRECTION ( 'NONE',  ( 1.000000000000000000, 0.000000000000000000, 0.000000000000000000 ) ) ;
#39890=ADVANCED_FACE ( 'NONE', ( #8142 ), #24086, .T. ) ;
#39892=CIRCLE ( 'NONE', #42401, 9.500000000000000000 ) ;
#39931=VECTOR ( 'NONE', #1275, 1000.000000000000114 ) ;
#39951=ORIENTED_EDGE ( 'NONE', *, *, #27971, .F. ) ;
#39954=EDGE_LOOP ( 'NONE', ( #1817, #13409, #49548, #31416, #21578 ) ) ;
#39960=DIRECTION ( 'NONE',  ( 0.000000000000000000, 0.000000000000000000, -1.000000000000000000 ) ) ;
#39973=CIRCLE ( 'NONE', #41650, 1.000000000000000888 ) ;
#40035=CARTESIAN_POINT ( 'NONE',  ( -21.36606260230379917, 21.88381105532059934, 11.84999999999999964 ) ) ;
#40046=CARTESIAN_POINT ( 'NONE',  ( 16.13393739769620083, -15.61618894467929941, -11.11999999999999922 ) ) ;
#40105=DIRECTION ( 'NONE',  ( 0.000000000000000000, 0.000000000000000000, -1.000000000000000000 ) ) ;
#40110=AXIS2_PLACEMENT_3D ( 'NONE', #49359, #14219, #37031 ) ;
#40130=DIRECTION ( 'NONE',  ( 0.7071067811865457964, 0.000000000000000000, -0.7071067811865492381 ) ) ;
#40136=LINE ( 'NONE', #45370, #36778 ) ;
#40140=EDGE_LOOP ( 'NONE', ( #25024, #47865 ) ) ;
#40152=CIRCLE ( 'NONE', #30062, 9.999999999999998224 ) ;
#40153=CARTESIAN_POINT ( 'NONE',  ( 53.63393739769619373, -63.11618894467929408, 16.35000000000000142 ) ) ;
#40155=CIRCLE ( 'NONE', #25047, 1.999999999999998224 ) ;
#40158=DIRECTION ( 'NONE',  ( 0.000000000000000000, 0.000000000000000000, 1.000000000000000000 ) ) ;
#40209=DIRECTION ( 'NONE',  ( 0.000000000000000000, 1.000000000000000000, 0.000000000000000000 ) ) ;
#40219=( GEOMETRIC_REPRESENTATION_CONTEXT ( 3 ) GLOBAL_UNCERTAINTY_ASSIGNED_CONTEXT ( ( #16914 ) ) GLOBAL_UNIT_ASSIGNED_CONTEXT ( ( #16560, #48285, #23884 ) ) REPRESENTATION_CONTEXT ( 'NONE', 'WORKASPACE' ) );
#40225=DIRECTION ( 'NONE',  ( -1.000000000000000000, 0.000000000000000000, 0.000000000000000000 ) ) ;
#40236=ORIENTED_EDGE ( 'NONE', *, *, #10066, .F. ) ;
#40248=DIRECTION ( 'NONE',  ( 1.000000000000000000, 0.000000000000000000, 0.000000000000000000 ) ) ;
#40261=ADVANCED_FACE ( 'NONE', ( #21651 ), #5492, .F. ) ;
#40267=VERTEX_POINT ( 'NONE', #49474 ) ;
#40289=ADVANCED_FACE ( 'NONE', ( #1756 ), #30603, .F. ) ;
#40299=AXIS2_PLACEMENT_3D ( 'NONE', #46606, #3090, #39505 ) ;
#40303=DIRECTION ( 'NONE',  ( 0.000000000000000000, 0.000000000000000000, 1.000000000000000000 ) ) ;
#40321=EDGE_CURVE ( 'NONE', #33500, #6443, #33196, .T. ) ;
#40325=CARTESIAN_POINT ( 'NONE',  ( 51.13393739769659874, -50.61618894467899565, 11.34999999999999964 ) ) ;
#40327=ORIENTED_EDGE ( 'NONE', *, *, #31558, .T. ) ;
#40333=CIRCLE ( 'NONE', #3500, 35.00000000000000000 ) ;
#40363=CARTESIAN_POINT ( 'NONE',  ( -21.36606260230379917, 31.59091783650714547, 11.14289321881345174 ) ) ;
#40386=DIRECTION ( 'NONE',  ( 0.000000000000000000, 1.000000000000000000, 0.000000000000000000 ) ) ;
#40410=EDGE_CURVE ( 'NONE', #33105, #23557, #18045, .T. ) ;
#40420=DIRECTION ( 'NONE',  ( 0.000000000000000000, 1.000000000000000000, 0.000000000000000000 ) ) ;
#40428=DIRECTION ( 'NONE',  ( -1.000000000000000000, 0.000000000000000000, 0.000000000000000000 ) ) ;
#40458=ORIENTED_EDGE ( 'NONE', *, *, #34724, .F. ) ;
#40470=CONICAL_SURFACE ( 'NONE', #30511, 1.079032500000000727, 0.7853981633974476129 ) ;
#40486=ORIENTED_EDGE ( 'NONE', *, *, #37070, .T. ) ;
#40539=DIRECTION ( 'NONE',  ( 0.000000000000000000, 0.000000000000000000, -1.000000000000000000 ) ) ;
#40553=CARTESIAN_POINT ( 'NONE',  ( 53.63393739769619373, -53.11618894467930119, 16.35000000000000142 ) ) ;
#40554=ORIENTED_EDGE ( 'NONE', *, *, #41269, .T. ) ;
#40558=DIRECTION ( 'NONE',  ( 0.000000000000000000, -1.000000000000000000, 0.000000000000000000 ) ) ;
#40562=AXIS2_PLACEMENT_3D ( 'NONE', #48410, #12512, #28478 ) ;
#40580=VERTEX_POINT ( 'NONE', #28557 ) ;
#40596=CARTESIAN_POINT ( 'NONE',  ( -21.36606260230379917, 30.88381105532059934, 10.84999999999999964 ) ) ;
#40597=DIRECTION ( 'NONE',  ( 1.000000000000000000, 0.000000000000000000, 0.000000000000000000 ) ) ;
#40621=DIRECTION ( 'NONE',  ( 0.000000000000000000, 0.000000000000000000, 1.000000000000000000 ) ) ;
#40622=LINE ( 'NONE', #4720, #38943 ) ;
#40629=ADVANCED_FACE ( 'NONE', ( #28818 ), #23075, .F. ) ;
#40642=VECTOR ( 'NONE', #34815, 1000.000000000000000 ) ;
#40657=ORIENTED_EDGE ( 'NONE', *, *, #18510, .T. ) ;
#40667=DIRECTION ( 'NONE',  ( 0.000000000000000000, 0.000000000000000000, -1.000000000000000000 ) ) ;
#40683=DIRECTION ( 'NONE',  ( 0.000000000000000000, 0.000000000000000000, 1.000000000000000000 ) ) ;
#40691=DIRECTION ( 'NONE',  ( -0.7071067811865475727, 0.7071067811865475727, 0.000000000000000000 ) ) ;
#40732=ORIENTED_EDGE ( 'NONE', *, *, #43960, .T. ) ;
#40794=DIRECTION ( 'NONE',  ( 0.000000000000000000, 0.000000000000000000, -1.000000000000000000 ) ) ;
#40802=DIRECTION ( 'NONE',  ( 1.000000000000000000, 0.000000000000000000, 0.000000000000000000 ) ) ;
#40825=DIRECTION ( 'NONE',  ( 0.000000000000000000, 0.000000000000000000, -1.000000000000000000 ) ) ;
#40841=ORIENTED_EDGE ( 'NONE', *, *, #9625, .T. ) ;
#40844=LINE ( 'NONE', #36133, #12323 ) ;
#40854=LINE ( 'NONE', #32973, #14573 ) ;
#40889=CIRCLE ( 'NONE', #24970, 1.000000000000000888 ) ;
#40905=DIRECTION ( 'NONE',  ( 0.000000000000000000, 0.000000000000000000, -1.000000000000000000 ) ) ;
#40954=DIRECTION ( 'NONE',  ( -1.000000000000000000, 0.000000000000000000, 0.000000000000000000 ) ) ;
#40964=CIRCLE ( 'NONE', #9178, 1.000000000000000888 ) ;
#40973=CIRCLE ( 'NONE', #7496, 1.000000000000000888 ) ;
#40989=EDGE_LOOP ( 'NONE', ( #11288, #10622, #3692, #30779, #28179 ) ) ;
#41042=VECTOR ( 'NONE', #41511, 1000.000000000000000 ) ;
#41048=ORIENTED_EDGE ( 'NONE', *, *, #14378, .T. ) ;
#41057=LINE ( 'NONE', #20343, #35979 ) ;
#41110=CARTESIAN_POINT ( 'NONE',  ( -31.36606260230380272, -62.11618894467930119, 11.84999999999999964 ) ) ;
#41126=AXIS2_PLACEMENT_3D ( 'NONE', #2120, #22535, #22790 ) ;
#41183=DIRECTION ( 'NONE',  ( 0.7071067811865473507, 0.7071067811865476838, 0.000000000000000000 ) ) ;
#41199=CIRCLE ( 'NONE', #18591, 6.000000000000000000 ) ;
#41211=DIRECTION ( 'NONE',  ( -0.5720614028176839172, 0.4156269377774525209, -0.7071067811865484609 ) ) ;
#41246=CARTESIAN_POINT ( 'NONE',  ( 16.13393739769620083, -15.61618894467929941, -14.68999999999999950 ) ) ;
#41269=EDGE_CURVE ( 'NONE', #20846, #25361, #49161, .T. ) ;
#41278=CIRCLE ( 'NONE', #10355, 18.00000000000000000 ) ;
#41293=DIRECTION ( 'NONE',  ( 0.000000000000000000, 0.000000000000000000, 1.000000000000000000 ) ) ;
#41298=EDGE_LOOP ( 'NONE', ( #33934, #14178, #1465, #23292, #46380 ) ) ;
#41301=CIRCLE ( 'NONE', #29580, 11.00000000000000000 ) ;
#41303=AXIS2_PLACEMENT_3D ( 'NONE', #244, #13346, #8892 ) ;
#41305=ORIENTED_EDGE ( 'NONE', *, *, #39280, .F. ) ;
#41310=FACE_OUTER_BOUND ( 'NONE', #39954, .T. ) ;
#41317=DIRECTION ( 'NONE',  ( 1.000000000000000000, 0.000000000000000000, 0.000000000000000000 ) ) ;
#41318=CIRCLE ( 'NONE', #47983, 11.00000000000000000 ) ;
#41343=VERTEX_POINT ( 'NONE', #42061 ) ;
#41353=DIRECTION ( 'NONE',  ( 1.260570937617230037E-11, 1.376914871200490071E-11, 1.000000000000000000 ) ) ;
#41355=VERTEX_POINT ( 'NONE', #22500 ) ;
#41356=EDGE_CURVE ( 'NONE', #14490, #6375, #7317, .T. ) ;
#41366=TOROIDAL_SURFACE ( 'NONE', #2888, 19.30901699437490038, 0.5000000000000000000 ) ;
#41379=DIRECTION ( 'NONE',  ( 0.000000000000000000, 0.000000000000000000, 1.000000000000000000 ) ) ;
#41390=EDGE_CURVE ( 'NONE', #13595, #16677, #18075, .T. ) ;
#41399=VECTOR ( 'NONE', #29462, 1000.000000000000000 ) ;
#41400=CARTESIAN_POINT ( 'NONE',  ( 54.36675628530522886, -55.06578241374116089, 16.85000000000000142 ) ) ;
#41424=CARTESIAN_POINT ( 'NONE',  ( 51.13393739769620083, -15.61618894467929941, 9.349999999999999645 ) ) ;
#41453=DIRECTION ( 'NONE',  ( 1.000000000000000000, 0.000000000000000000, 0.000000000000000000 ) ) ;
#41454=ADVANCED_FACE ( 'NONE', ( #46649 ), #30633, .F. ) ;
#41455=DIRECTION ( 'NONE',  ( -1.000000000000000000, 0.000000000000000000, 0.000000000000000000 ) ) ;
#41466=AXIS2_PLACEMENT_3D ( 'NONE', #42376, #33963, #14071 ) ;
#41477=DIRECTION ( 'NONE',  ( 0.000000000000000000, 1.000000000000000000, 0.000000000000000000 ) ) ;
#41480=CARTESIAN_POINT ( 'NONE',  ( -21.36606260230379917, 21.88381105532059934, 11.84999999999999964 ) ) ;
#41506=VECTOR ( 'NONE', #29724, 1000.000000000000114 ) ;
#41511=DIRECTION ( 'NONE',  ( 0.000000000000000000, 1.000000000000000000, 0.000000000000000000 ) ) ;
#41532=CARTESIAN_POINT ( 'NONE',  ( 2.633937397696199945, -15.61618894467930119, 4.349999999999999645 ) ) ;
#41535=CARTESIAN_POINT ( 'NONE',  ( -18.35638189584738100, -50.24588423573534612, 11.97999999999999865 ) ) ;
#41538=EDGE_CURVE ( 'NONE', #22408, #40267, #43201, .T. ) ;
#41579=DIRECTION ( 'NONE',  ( 0.000000000000000000, 0.000000000000000000, 1.000000000000000000 ) ) ;
#41582=CARTESIAN_POINT ( 'NONE',  ( -21.36606260230379917, -53.11618894467930119, 17.35000000000000142 ) ) ;
#41584=ADVANCED_FACE ( 'NONE', ( #28235 ), #25614, .T. ) ;
#41588=CARTESIAN_POINT ( 'NONE',  ( 16.13393739769620083, -15.61618894467929941, -14.03562394879499919 ) ) ;
#41590=FACE_OUTER_BOUND ( 'NONE', #9542, .T. ) ;
#41601=DIRECTION ( 'NONE',  ( -1.000000000000000000, 0.000000000000000000, 0.000000000000000000 ) ) ;
#41615=FACE_OUTER_BOUND ( 'NONE', #7203, .T. ) ;
#41627=DIRECTION ( 'NONE',  ( 0.000000000000000000, 0.000000000000000000, -1.000000000000000000 ) ) ;
#41628=ORIENTED_EDGE ( 'NONE', *, *, #34110, .T. ) ;
#41650=AXIS2_PLACEMENT_3D ( 'NONE', #42261, #14218, #10027 ) ;
#41698=CARTESIAN_POINT ( 'NONE',  ( 63.34104417888273986, -39.36618894467940066, 17.05710678118654755 ) ) ;
#41716=CIRCLE ( 'NONE', #48417, 5.999999999999998224 ) ;
#41727=CARTESIAN_POINT ( 'NONE',  ( 51.64361810415240939, 19.01350634637644532, 16.21999999999999886 ) ) ;
#41728=EDGE_LOOP ( 'NONE', ( #40486, #33874, #20267, #48532, #33685 ) ) ;
#41758=DIRECTION ( 'NONE',  ( 0.7071067811865473507, 0.7071067811865476838, 0.000000000000000000 ) ) ;
#41792=CONICAL_SURFACE ( 'NONE', #40110, 1.079032500000000727, 0.7853981633974476129 ) ;
#41802=DIRECTION ( 'NONE',  ( -0.8090169943749462300, -0.5877852522924749135, 0.000000000000000000 ) ) ;
#41839=EDGE_CURVE ( 'NONE', #34457, #5441, #6941, .T. ) ;
#41848=DIRECTION ( 'NONE',  ( 0.000000000000000000, 0.000000000000000000, -1.000000000000000000 ) ) ;
#41862=ORIENTED_EDGE ( 'NONE', *, *, #13620, .F. ) ;
#41869=AXIS2_PLACEMENT_3D ( 'NONE', #2955, #10041, #34387 ) ;
#41871=CIRCLE ( 'NONE', #6755, 5.499999999999998224 ) ;
#41877=ORIENTED_EDGE ( 'NONE', *, *, #22759, .T. ) ;
#41881=DIRECTION ( 'NONE',  ( 0.8090169943749472292, -0.5877852522924734702, 0.000000000000000000 ) ) ;
#41886=ORIENTED_EDGE ( 'NONE', *, *, #27679, .T. ) ;
#41964=DIRECTION ( 'NONE',  ( 0.000000000000000000, 0.000000000000000000, 1.000000000000000000 ) ) ;
#41995=DIRECTION ( 'NONE',  ( 0.5720614028176828070, -0.4156269377774550189, -0.7071067811865477948 ) ) ;
#42003=CARTESIAN_POINT ( 'NONE',  ( -18.49575789335964160, 18.87413034886438368, 11.97999999999999865 ) ) ;
#42007=CARTESIAN_POINT ( 'NONE',  ( 51.13393739769659874, -50.61618894467899565, 16.85000000000000142 ) ) ;
#42020=VERTEX_POINT ( 'NONE', #20765 ) ;
#42022=EDGE_CURVE ( 'NONE', #39126, #28421, #44086, .T. ) ;
#42061=CARTESIAN_POINT ( 'NONE',  ( 63.63393739769619373, -53.11618894467930119, 16.35000000000000142 ) ) ;
#42076=DIRECTION ( 'NONE',  ( 0.000000000000000000, 0.000000000000000000, 1.000000000000000000 ) ) ;
#42077=ORIENTED_EDGE ( 'NONE', *, *, #34787, .T. ) ;
#42090=AXIS2_PLACEMENT_3D ( 'NONE', #7135, #25987, #50118 ) ;
#42103=DIRECTION ( 'NONE',  ( 0.000000000000000000, 0.000000000000000000, 1.000000000000000000 ) ) ;
#42138=ORIENTED_EDGE ( 'NONE', *, *, #11590, .F. ) ;
#42155=AXIS2_PLACEMENT_3D ( 'NONE', #1102, #36733, #20481 ) ;
#42162=ADVANCED_FACE ( 'NONE', ( #34631 ), #27319, .F. ) ;
#42175=EDGE_LOOP ( 'NONE', ( #10660, #426, #49864, #17501 ) ) ;
#42180=LINE ( 'NONE', #2339, #3075 ) ;
#42182=EDGE_CURVE ( 'NONE', #727, #22408, #42259, .T. ) ;
#42194=ORIENTED_EDGE ( 'NONE', *, *, #41538, .T. ) ;
#42206=EDGE_CURVE ( 'NONE', #29477, #2118, #9775, .T. ) ;
#42220=DIRECTION ( 'NONE',  ( 1.224650706428208818E-16, 1.000000000000000000, 8.281540456132313294E-12 ) ) ;
#42223=ORIENTED_EDGE ( 'NONE', *, *, #44104, .T. ) ;
#42224=CARTESIAN_POINT ( 'NONE',  ( -13.36606260230359844, -50.61618894467959962, 11.34999999999999964 ) ) ;
#42253=FACE_OUTER_BOUND ( 'NONE', #24974, .T. ) ;
#42259=LINE ( 'NONE', #26509, #9748 ) ;
#42261=CARTESIAN_POINT ( 'NONE',  ( 62.63393739769619373, -53.11618894467930119, 11.84999999999999964 ) ) ;
#42268=CARTESIAN_POINT ( 'NONE',  ( 53.63393739769619373, 21.88381105532059934, 16.35000000000000142 ) ) ;
#42279=EDGE_LOOP ( 'NONE', ( #21501, #44710, #9862, #44504 ) ) ;
#42283=VERTEX_POINT ( 'NONE', #2685 ) ;
#42290=FACE_OUTER_BOUND ( 'NONE', #50206, .T. ) ;
#42293=VERTEX_POINT ( 'NONE', #14732 ) ;
#42299=EDGE_CURVE ( 'NONE', #16350, #9032, #47427, .T. ) ;
#42312=CIRCLE ( 'NONE', #37293, 5.500000000000000000 ) ;
#42317=CARTESIAN_POINT ( 'NONE',  ( 62.63393739769619373, 21.88381105532059934, 11.84999999999999964 ) ) ;
#42361=DIRECTION ( 'NONE',  ( 1.000000000000000000, 0.000000000000000000, 0.000000000000000000 ) ) ;
#42369=EDGE_CURVE ( 'NONE', #42020, #1082, #25406, .T. ) ;
#42372=PRESENTATION_STYLE_ASSIGNMENT (( #26355 ) ) ;
#42374=ADVANCED_FACE ( 'NONE', ( #9959 ), #2221, .F. ) ;
#42376=CARTESIAN_POINT ( 'NONE',  ( -30.36606260230379917, 8.133811055320650851, 16.35000000000000142 ) ) ;
#42384=EDGE_LOOP ( 'NONE', ( #50781, #22862 ) ) ;
#42391=CARTESIAN_POINT ( 'NONE',  ( 16.13393739769620083, -15.61618894467929941, -15.18999999999999950 ) ) ;
#42397=DIRECTION ( 'NONE',  ( 1.000000000000000000, 5.495516945195724241E-29, 2.619602780254359830E-11 ) ) ;
#42401=AXIS2_PLACEMENT_3D ( 'NONE', #46407, #22520, #2885 ) ;
#42415=ADVANCED_FACE ( 'NONE', ( #42980 ), #35351, .T. ) ;
#42439=ORIENTED_EDGE ( 'NONE', *, *, #43709, .T. ) ;
#42446=VECTOR ( 'NONE', #48194, 1000.000000000000000 ) ;
#42447=DIRECTION ( 'NONE',  ( 1.260570937617230037E-11, 1.376914871200490071E-11, 1.000000000000000000 ) ) ;
#42466=DIRECTION ( 'NONE',  ( 0.000000000000000000, 0.000000000000000000, -1.000000000000000000 ) ) ;
#42477=VERTEX_POINT ( 'NONE', #14925 ) ;
#42488=VERTEX_POINT ( 'NONE', #26971 ) ;
#42510=CARTESIAN_POINT ( 'NONE',  ( 16.13393739769620083, -15.61618894467929941, -20.58999999999999986 ) ) ;
#42519=VERTEX_POINT ( 'NONE', #35555 ) ;
#42550=ADVANCED_FACE ( 'NONE', ( #35021 ), #42914, .T. ) ;
#42591=EDGE_CURVE ( 'NONE', #42921, #26465, #13176, .T. ) ;
#42598=DIRECTION ( 'NONE',  ( 0.000000000000000000, 0.000000000000000000, 1.000000000000000000 ) ) ;
#42607=CARTESIAN_POINT ( 'NONE',  ( 16.13393739769620083, -15.61618894467929941, -5.966499999999999915 ) ) ;
#42612=ADVANCED_FACE ( 'NONE', ( #30826 ), #45774, .F. ) ;
#42653=CARTESIAN_POINT ( 'NONE',  ( 16.13393739769620083, -15.61618894467929941, -20.58999999999999986 ) ) ;
#42670=VERTEX_POINT ( 'NONE', #6696 ) ;
#42698=ORIENTED_EDGE ( 'NONE', *, *, #51590, .F. ) ;
#42751=CARTESIAN_POINT ( 'NONE',  ( -31.36606260230380272, -62.82329572586585442, 11.14289321881345174 ) ) ;
#42814=FACE_BOUND ( 'NONE', #49636, .T. ) ;
#42823=VECTOR ( 'NONE', #50831, 1000.000000000000000 ) ;
#42825=DIRECTION ( 'NONE',  ( 0.000000000000000000, 0.000000000000000000, 1.000000000000000000 ) ) ;
#42847=DIRECTION ( 'NONE',  ( -1.000000000000000000, 0.000000000000000000, 0.000000000000000000 ) ) ;
#42868=CARTESIAN_POINT ( 'NONE',  ( 16.13393739769620083, -15.61618894467929941, -5.966499999999999915 ) ) ;
#42871=EDGE_LOOP ( 'NONE', ( #21365, #41862, #4247, #47541, #2380, #687, #35530, #27155 ) ) ;
#42875=CARTESIAN_POINT ( 'NONE',  ( 25.63393739769619728, -15.61618894467930119, -18.35000000000000142 ) ) ;
#42884=EDGE_CURVE ( 'NONE', #32800, #44094, #32694, .T. ) ;
#42885=DIRECTION ( 'NONE',  ( 0.000000000000000000, 0.000000000000000000, -1.000000000000000000 ) ) ;
#42914=PLANE ( 'NONE',  #30717 ) ;
#42921=VERTEX_POINT ( 'NONE', #8110 ) ;
#42939=DIRECTION ( 'NONE',  ( 0.000000000000000000, 0.000000000000000000, -1.000000000000000000 ) ) ;
#42944=EDGE_CURVE ( 'NONE', #8804, #17463, #24571, .T. ) ;
#42947=DIRECTION ( 'NONE',  ( -1.000000000000000000, 0.000000000000000000, 0.000000000000000000 ) ) ;
#42948=EDGE_CURVE ( 'NONE', #12281, #32578, #28258, .T. ) ;
#42964=LINE ( 'NONE', #13880, #40642 ) ;
#42980=FACE_OUTER_BOUND ( 'NONE', #33165, .T. ) ;
#42984=CYLINDRICAL_SURFACE ( 'NONE', #48227, 9.999999999999998224 ) ;
#42994=DIRECTION ( 'NONE',  ( 0.000000000000000000, 0.000000000000000000, 1.000000000000000000 ) ) ;
#42996=ORIENTED_EDGE ( 'NONE', *, *, #10408, .T. ) ;
#42998=ORIENTED_EDGE ( 'NONE', *, *, #41839, .F. ) ;
#43006=ORIENTED_EDGE ( 'NONE', *, *, #51438, .T. ) ;
#43023=DIRECTION ( 'NONE',  ( 1.000000000000000000, 0.000000000000000000, 0.000000000000000000 ) ) ;
#43024=FACE_OUTER_BOUND ( 'NONE', #28362, .T. ) ;
#43060=LINE ( 'NONE', #34651, #16193 ) ;
#43067=ORIENTED_EDGE ( 'NONE', *, *, #42369, .T. ) ;
#43073=EDGE_CURVE ( 'NONE', #235, #11148, #40844, .T. ) ;
#43074=CARTESIAN_POINT ( 'NONE',  ( 16.13393739769620083, -15.61618894467929941, 14.34999999999999964 ) ) ;
#43081=CARTESIAN_POINT ( 'NONE',  ( -21.36606260230379917, 30.88381105532059934, 16.35000000000000142 ) ) ;
#43112=ORIENTED_EDGE ( 'NONE', *, *, #26461, .T. ) ;
#43156=AXIS2_PLACEMENT_3D ( 'NONE', #6093, #14462, #50112 ) ;
#43157=DIRECTION ( 'NONE',  ( 0.000000000000000000, 0.000000000000000000, -1.000000000000000000 ) ) ;
#43163=EDGE_LOOP ( 'NONE', ( #21426, #48526, #39412, #28879 ) ) ;
#43193=CARTESIAN_POINT ( 'NONE',  ( -21.36606260230379917, 31.88381105532059934, 16.35000000000000142 ) ) ;
#43194=ADVANCED_FACE ( 'NONE', ( #41615 ), #49965, .F. ) ;
#43201=CIRCLE ( 'NONE', #47396, 1.000000000000000888 ) ;
#43217=FACE_OUTER_BOUND ( 'NONE', #28404, .T. ) ;
#43222=AXIS2_PLACEMENT_3D ( 'NONE', #47940, #43998, #4161 ) ;
#43282=FACE_OUTER_BOUND ( 'NONE', #34869, .T. ) ;
#43311=CARTESIAN_POINT ( 'NONE',  ( -18.86606260230360022, -50.61618894467959962, 11.34999999999999964 ) ) ;
#43327=ORIENTED_EDGE ( 'NONE', *, *, #51008, .T. ) ;
#43352=CARTESIAN_POINT ( 'NONE',  ( -30.36606260230379917, -53.11618894467940066, 16.35000000000000142 ) ) ;
#43382=AXIS2_PLACEMENT_3D ( 'NONE', #13107, #36395, #49257 ) ;
#43405=CARTESIAN_POINT ( 'NONE',  ( 16.13393739769620083, -15.61618894467929941, 14.62639320225000006 ) ) ;
#43429=ORIENTED_EDGE ( 'NONE', *, *, #22003, .F. ) ;
#43455=CARTESIAN_POINT ( 'NONE',  ( -18.86606260230390220, 19.38381105532060289, 16.85000000000000142 ) ) ;
#43478=AXIS2_PLACEMENT_3D ( 'NONE', #28274, #13108, #29059 ) ;
#43518=AXIS2_PLACEMENT_3D ( 'NONE', #33713, #37923, #2538 ) ;
#43521=EDGE_LOOP ( 'NONE', ( #15830, #40458, #7104, #11840, #27850, #39587 ) ) ;
#43522=ORIENTED_EDGE ( 'NONE', *, *, #23858, .F. ) ;
#43523=AXIS2_PLACEMENT_3D ( 'NONE', #28917, #22085, #29441 ) ;
#43544=DIRECTION ( 'NONE',  ( -8.660081000000000658E-17, -2.123755000000000144E-17, -1.000000000000000000 ) ) ;
#43596=CIRCLE ( 'NONE', #87, 28.27108544675919788 ) ;
#43626=DIRECTION ( 'NONE',  ( 0.5720614028176831400, -0.4156269377774557405, -0.7071067811865470176 ) ) ;
#43709=EDGE_CURVE ( 'NONE', #16578, #34913, #51682, .T. ) ;
#43718=ADVANCED_FACE ( 'NONE', ( #339 ), #17111, .T. ) ;
#43721=FACE_OUTER_BOUND ( 'NONE', #17393, .T. ) ;
#43731=DIRECTION ( 'NONE',  ( 0.000000000000000000, 0.000000000000000000, -1.000000000000000000 ) ) ;
#43739=DIRECTION ( 'NONE',  ( 0.000000000000000000, 1.000000000000000000, 0.000000000000000000 ) ) ;
#43760=ORIENTED_EDGE ( 'NONE', *, *, #19864, .F. ) ;
#43764=EDGE_LOOP ( 'NONE', ( #27986, #17424 ) ) ;
#43766=CARTESIAN_POINT ( 'NONE',  ( -8.866062602303902196, -15.61618894467929941, 7.919999999999963514 ) ) ;
#43768=CARTESIAN_POINT ( 'NONE',  ( 53.63393739769619373, 30.88381105532059934, 17.35000000000000142 ) ) ;
#43788=AXIS2_PLACEMENT_3D ( 'NONE', #44845, #40905, #8950 ) ;
#43812=CARTESIAN_POINT ( 'NONE',  ( -18.86606260230360022, -50.61618894467959962, 10.84999999999999964 ) ) ;
#43820=CARTESIAN_POINT ( 'NONE',  ( -3.175079596678700433, -15.61618894467929941, 16.85000000000000142 ) ) ;
#43829=ORIENTED_EDGE ( 'NONE', *, *, #5051, .T. ) ;
#43847=CARTESIAN_POINT ( 'NONE',  ( -0.9360626029568490658, -15.61618894436409732, -14.69000000030820985 ) ) ;
#43857=ORIENTED_EDGE ( 'NONE', *, *, #23985, .F. ) ;
#43884=AXIS2_PLACEMENT_3D ( 'NONE', #27597, #47539, #11635 ) ;
#43896=AXIS2_PLACEMENT_3D ( 'NONE', #28479, #8067, #28216 ) ;
#43922=DIRECTION ( 'NONE',  ( 0.000000000000000000, 0.000000000000000000, -1.000000000000000000 ) ) ;
#43960=EDGE_CURVE ( 'NONE', #42020, #32963, #21540, .T. ) ;
#43963=CARTESIAN_POINT ( 'NONE',  ( -18.86606260230360022, -50.61618894467959962, 16.85000000000000142 ) ) ;
#43989=AXIS2_PLACEMENT_3D ( 'NONE', #14611, #26128, #22195 ) ;
#43991=CARTESIAN_POINT ( 'NONE',  ( -18.49575789335964515, 19.89349176177682210, 16.21999999999999886 ) ) ;
#43998=DIRECTION ( 'NONE',  ( -1.000000000000000000, 0.000000000000000000, 0.000000000000000000 ) ) ;
#44003=ORIENTED_EDGE ( 'NONE', *, *, #31307, .T. ) ;
#44014=AXIS2_PLACEMENT_3D ( 'NONE', #19355, #47159, #11246 ) ;
#44021=LINE ( 'NONE', #15724, #29591 ) ;
#44025=DIRECTION ( 'NONE',  ( 0.000000000000000000, 0.000000000000000000, 1.000000000000000000 ) ) ;
#44086=CIRCLE ( 'NONE', #28156, 4.649999999999999467 ) ;
#44089=AXIS2_PLACEMENT_3D ( 'NONE', #17866, #26491, #33837 ) ;
#44093=EDGE_CURVE ( 'NONE', #42488, #50414, #32405, .T. ) ;
#44094=VERTEX_POINT ( 'NONE', #10215 ) ;
#44098=CIRCLE ( 'NONE', #45789, 17.06999999999999673 ) ;
#44104=EDGE_CURVE ( 'NONE', #45507, #12281, #50892, .T. ) ;
#44106=ORIENTED_EDGE ( 'NONE', *, *, #14566, .F. ) ;
#44136=VERTEX_POINT ( 'NONE', #45077 ) ;
#44140=EDGE_LOOP ( 'NONE', ( #38807, #4971 ) ) ;
#44149=CARTESIAN_POINT ( 'NONE',  ( 5.133937397847174289, -15.61618894439989802, -19.08999999999999986 ) ) ;
#44151=ORIENTED_EDGE ( 'NONE', *, *, #34697, .T. ) ;
#44157=DIRECTION ( 'NONE',  ( -0.7071067811865475727, 0.7071067811865475727, 0.000000000000000000 ) ) ;
#44185=AXIS2_PLACEMENT_3D ( 'NONE', #40046, #40303, #208 ) ;
#44231=ADVANCED_FACE ( 'NONE', ( #43721 ), #4137, .T. ) ;
#44239=VERTEX_POINT ( 'NONE', #4395 ) ;
#44252=ORIENTED_EDGE ( 'NONE', *, *, #34697, .F. ) ;
#44262=CIRCLE ( 'NONE', #25827, 13.50000000000000178 ) ;
#44279=CYLINDRICAL_SURFACE ( 'NONE', #4105, 5.499999999999998224 ) ;
#44284=DIRECTION ( 'NONE',  ( 0.000000000000000000, 0.000000000000000000, -1.000000000000000000 ) ) ;
#44291=DIRECTION ( 'NONE',  ( 0.000000000000000000, 1.000000000000000000, 0.000000000000000000 ) ) ;
#44316=EDGE_CURVE ( 'NONE', #17150, #15443, #45014, .T. ) ;
#44319=CARTESIAN_POINT ( 'NONE',  ( 34.99574079657120507, -15.61618894467929763, 17.07360679774999923 ) ) ;
#44339=CIRCLE ( 'NONE', #34249, 10.00000000000000888 ) ;
#44340=LINE ( 'NONE', #40153, #22627 ) ;
#44366=AXIS2_PLACEMENT_3D ( 'NONE', #41246, #1416, #21832 ) ;
#44375=CARTESIAN_POINT ( 'NONE',  ( 16.13393739769620083, -15.61618894467929941, -18.35000000000000142 ) ) ;
#44376=VECTOR ( 'NONE', #2195, 1000.000000000000000 ) ;
#44385=EDGE_CURVE ( 'NONE', #8558, #11901, #35513, .T. ) ;
#44388=EDGE_LOOP ( 'NONE', ( #21616, #51295 ) ) ;
#44399=FACE_OUTER_BOUND ( 'NONE', #27769, .T. ) ;
#44405=CARTESIAN_POINT ( 'NONE',  ( -21.36606260230379917, -62.11618894467930119, 11.84999999999999964 ) ) ;
#44417=AXIS2_PLACEMENT_3D ( 'NONE', #25611, #26134, #21430 ) ;
#44425=ORIENTED_EDGE ( 'NONE', *, *, #22759, .F. ) ;
#44456=DIRECTION ( 'NONE',  ( -1.000000000000000000, 0.000000000000000000, 0.000000000000000000 ) ) ;
#44466=FACE_OUTER_BOUND ( 'NONE', #13903, .T. ) ;
#44472=DIRECTION ( 'NONE',  ( -1.000000000000000000, 0.000000000000000000, 0.000000000000000000 ) ) ;
#44473=CARTESIAN_POINT ( 'NONE',  ( 54.66064891145139626, -45.76208697842928785, 10.84999999999999964 ) ) ;
#44481=AXIS2_PLACEMENT_3D ( 'NONE', #41588, #17996, #9626 ) ;
#44504=ORIENTED_EDGE ( 'NONE', *, *, #11071, .T. ) ;
#44514=ORIENTED_EDGE ( 'NONE', *, *, #41390, .F. ) ;
#44531=EDGE_CURVE ( 'NONE', #33105, #44858, #36015, .T. ) ;
#44545=FACE_OUTER_BOUND ( 'NONE', #23169, .T. ) ;
#44558=CARTESIAN_POINT ( 'NONE',  ( 16.13393739769620083, -15.61618894467929941, 14.62639320225000006 ) ) ;
#44608=ADVANCED_FACE ( 'NONE', ( #28141 ), #47531, .T. ) ;
#44613=DIRECTION ( 'NONE',  ( 0.000000000000000000, 0.000000000000000000, -1.000000000000000000 ) ) ;
#44616=VERTEX_POINT ( 'NONE', #42224 ) ;
#44620=CARTESIAN_POINT ( 'NONE',  ( 50.76363268875235235, -50.10650823822278710, 11.97999999999999865 ) ) ;
#44648=ORIENTED_EDGE ( 'NONE', *, *, #14607, .T. ) ;
#44666=ORIENTED_EDGE ( 'NONE', *, *, #452, .F. ) ;
#44678=DIRECTION ( 'NONE',  ( 0.000000000000000000, 0.000000000000000000, -1.000000000000000000 ) ) ;
#44696=CIRCLE ( 'NONE', #16235, 1.000000000000000888 ) ;
#44708=ORIENTED_EDGE ( 'NONE', *, *, #3477, .F. ) ;
#44710=ORIENTED_EDGE ( 'NONE', *, *, #48165, .F. ) ;
#44712=VERTEX_POINT ( 'NONE', #26732 ) ;
#44722=CARTESIAN_POINT ( 'NONE',  ( 60.70500520956166923, 28.95487886718607484, 16.35000000000000142 ) ) ;
#44725=AXIS2_PLACEMENT_3D ( 'NONE', #20223, #51698, #24397 ) ;
#44734=VECTOR ( 'NONE', #12795, 1000.000000000000000 ) ;
#44746=ORIENTED_EDGE ( 'NONE', *, *, #44753, .T. ) ;
#44753=EDGE_CURVE ( 'NONE', #50005, #24458, #1547, .T. ) ;
#44757=AXIS2_PLACEMENT_3D ( 'NONE', #33443, #16438, #41317 ) ;
#44765=VERTEX_POINT ( 'NONE', #11289 ) ;
#44794=ORIENTED_EDGE ( 'NONE', *, *, #20385, .F. ) ;
#44796=CARTESIAN_POINT ( 'NONE',  ( -18.86606260230360022, -50.61618894467959962, 11.97999999999999865 ) ) ;
#44801=AXIS2_PLACEMENT_3D ( 'NONE', #32204, #7881, #8647 ) ;
#44816=PLANE ( 'NONE',  #4947 ) ;
#44825=ADVANCED_FACE ( 'NONE', ( #17280, #49000 ), #19901, .T. ) ;
#44845=CARTESIAN_POINT ( 'NONE',  ( 16.13393739769620083, -15.61618894467929941, 17.07360679774999923 ) ) ;
#44858=VERTEX_POINT ( 'NONE', #24586 ) ;
#44859=DIRECTION ( 'NONE',  ( 0.000000000000000000, 0.000000000000000000, -1.000000000000000000 ) ) ;
#44887=CYLINDRICAL_SURFACE ( 'NONE', #48293, 10.00000000000000888 ) ;
#44891=CIRCLE ( 'NONE', #49067, 6.100000000000001421 ) ;
#44905=VERTEX_POINT ( 'NONE', #40596 ) ;
#44906=DIRECTION ( 'NONE',  ( 0.000000000000000000, 0.000000000000000000, 1.000000000000000000 ) ) ;
#44917=EDGE_LOOP ( 'NONE', ( #38118, #29675, #11791, #50716, #37558 ) ) ;
#44925=ORIENTED_EDGE ( 'NONE', *, *, #3906, .F. ) ;
#44927=ORIENTED_EDGE ( 'NONE', *, *, #43073, .T. ) ;
#44969=DIRECTION ( 'NONE',  ( -1.000000000000000000, 0.000000000000000000, 0.000000000000000000 ) ) ;
#44984=CARTESIAN_POINT ( 'NONE',  ( -30.36606260230379917, 8.133811055320650851, 16.35000000000000142 ) ) ;
#44998=LINE ( 'NONE', #8585, #32197 ) ;
#45003=DIRECTION ( 'NONE',  ( 1.000000000000000000, 0.000000000000000000, 0.000000000000000000 ) ) ;
#45014=CIRCLE ( 'NONE', #44185, 13.50000000000000178 ) ;
#45050=CARTESIAN_POINT ( 'NONE',  ( -21.36606260230379917, -53.11618894467930119, 11.84999999999999964 ) ) ;
#45058=EDGE_CURVE ( 'NONE', #20846, #25261, #24929, .T. ) ;
#45067=CARTESIAN_POINT ( 'NONE',  ( 16.13393739769620083, 30.88381105532059934, 11.84999999999999964 ) ) ;
#45077=CARTESIAN_POINT ( 'NONE',  ( 56.63393739769620083, 19.38381105532069881, 16.85000000000000142 ) ) ;
#45082=ORIENTED_EDGE ( 'NONE', *, *, #5385, .T. ) ;
#45098=ORIENTED_EDGE ( 'NONE', *, *, #46075, .T. ) ;
#45106=FACE_OUTER_BOUND ( 'NONE', #2958, .T. ) ;
#45109=ORIENTED_EDGE ( 'NONE', *, *, #43073, .F. ) ;
#45116=CARTESIAN_POINT ( 'NONE',  ( 16.13393739769620083, -15.61618894467929941, -2.149999999999999911 ) ) ;
#45128=ADVANCED_FACE ( 'NONE', ( #47896 ), #38366, .F. ) ;
#45134=AXIS2_PLACEMENT_3D ( 'NONE', #45116, #29377, #45378 ) ;
#45172=ORIENTED_EDGE ( 'NONE', *, *, #26592, .F. ) ;
#45174=AXIS2_PLACEMENT_3D ( 'NONE', #43311, #7403, #31989 ) ;
#45201=AXIS2_PLACEMENT_3D ( 'NONE', #27306, #51175, #7152 ) ;
#45206=EDGE_CURVE ( 'NONE', #24197, #16397, #46766, .T. ) ;
#45221=DIRECTION ( 'NONE',  ( -0.7071067811865476838, -0.7071067811865473507, 0.000000000000000000 ) ) ;
#45233=CARTESIAN_POINT ( 'NONE',  ( -31.36606260230380272, -53.11618894467930119, 16.35000000000000142 ) ) ;
#45234=CARTESIAN_POINT ( 'NONE',  ( 60.70500520956167634, 28.95487886718607839, 17.35000000000000142 ) ) ;
#45238=ORIENTED_EDGE ( 'NONE', *, *, #33909, .T. ) ;
#45253=DIRECTION ( 'NONE',  ( 0.5720614028176843613, 0.4156269377774527984, 0.7071067811865479058 ) ) ;
#45301=DIRECTION ( 'NONE',  ( 0.000000000000000000, -0.7071067811865492381, 0.7071067811865457964 ) ) ;
#45341=DIRECTION ( 'NONE',  ( 0.7071067811865475727, -0.7071067811865475727, 0.000000000000000000 ) ) ;
#45350=AXIS2_PLACEMENT_3D ( 'NONE', #29928, #10300, #26001 ) ;
#45351=EDGE_CURVE ( 'NONE', #45801, #32578, #41716, .T. ) ;
#45355=VECTOR ( 'NONE', #45253, 1000.000000000000000 ) ;
#45370=CARTESIAN_POINT ( 'NONE',  ( 11.48393739769620048, -15.61618894467929941, -14.03562394879499919 ) ) ;
#45378=DIRECTION ( 'NONE',  ( -1.000000000000000000, 0.000000000000000000, 0.000000000000000000 ) ) ;
#45388=EDGE_CURVE ( 'NONE', #3175, #17463, #3240, .T. ) ;
#45400=DIRECTION ( 'NONE',  ( 0.000000000000000000, 0.000000000000000000, -1.000000000000000000 ) ) ;
#45401=DIRECTION ( 'NONE',  ( 0.000000000000000000, 0.000000000000000000, -1.000000000000000000 ) ) ;
#45414=EDGE_CURVE ( 'NONE', #24458, #33328, #19158, .T. ) ;
#45427=DIRECTION ( 'NONE',  ( 0.000000000000000000, 0.000000000000000000, 1.000000000000000000 ) ) ;
#45477=AXIS2_PLACEMENT_3D ( 'NONE', #42268, #9273, #17892 ) ;
#45499=EDGE_LOOP ( 'NONE', ( #50925, #24318, #9922, #28922 ) ) ;
#45504=DIRECTION ( 'NONE',  ( 0.000000000000000000, 0.000000000000000000, 1.000000000000000000 ) ) ;
#45507=VERTEX_POINT ( 'NONE', #13798 ) ;
#45519=AXIS2_PLACEMENT_3D ( 'NONE', #9420, #20405, #49511 ) ;
#45525=LINE ( 'NONE', #26098, #22614 ) ;
#45532=AXIS2_PLACEMENT_3D ( 'NONE', #39798, #47669, #3904 ) ;
#45565=CARTESIAN_POINT ( 'NONE',  ( 16.13393739667419879, -15.61618894434099936, -11.12000000014429979 ) ) ;
#45566=CIRCLE ( 'NONE', #7892, 5.499999999999998224 ) ;
#45594=CARTESIAN_POINT ( 'NONE',  ( -18.86606260230360022, -50.61618894467959962, 11.97999999999999865 ) ) ;
#45636=CIRCLE ( 'NONE', #15520, 10.00000000000000355 ) ;
#45647=ORIENTED_EDGE ( 'NONE', *, *, #23985, .T. ) ;
#45657=ORIENTED_EDGE ( 'NONE', *, *, #21791, .F. ) ;
#45677=CARTESIAN_POINT ( 'NONE',  ( -30.36606260230379917, -15.61618894467929941, 11.84999999999999964 ) ) ;
#45678=VECTOR ( 'NONE', #26819, 1000.000000000000000 ) ;
#45693=ORIENTED_EDGE ( 'NONE', *, *, #48099, .F. ) ;
#45707=CIRCLE ( 'NONE', #33107, 6.000000000000000000 ) ;
#45710=LINE ( 'NONE', #5624, #41042 ) ;
#45723=ORIENTED_EDGE ( 'NONE', *, *, #27539, .T. ) ;
#45746=EDGE_LOOP ( 'NONE', ( #5826, #46744, #7071, #44514 ) ) ;
#45764=CIRCLE ( 'NONE', #18141, 0.4999999999999987232 ) ;
#45774=TOROIDAL_SURFACE ( 'NONE', #8970, 10.49999999968949815, 0.4999999999856510335 ) ;
#45789=AXIS2_PLACEMENT_3D ( 'NONE', #9103, #708, #45003 ) ;
#45795=EDGE_CURVE ( 'NONE', #44136, #18843, #22477, .T. ) ;
#45801=VERTEX_POINT ( 'NONE', #8773 ) ;
#45804=PRODUCT_DEFINITION_SHAPE ( 'NONE', 'NONE',  #15826 ) ;
#45820=CARTESIAN_POINT ( 'NONE',  ( 16.13393739769620083, -15.61618894467929941, -9.392532499999980189 ) ) ;
#45823=ORIENTED_EDGE ( 'NONE', *, *, #47575, .T. ) ;
#45825=DIRECTION ( 'NONE',  ( 0.000000000000000000, 0.000000000000000000, 1.000000000000000000 ) ) ;
#45835=DIRECTION ( 'NONE',  ( 0.000000000000000000, 0.000000000000000000, -1.000000000000000000 ) ) ;
#45863=DIRECTION ( 'NONE',  ( 0.000000000000000000, 1.000000000000000000, 0.000000000000000000 ) ) ;
#45939=CARTESIAN_POINT ( 'NONE',  ( 35.44295439207109411, -15.61618894467929763, 16.85000000000000142 ) ) ;
#45940=CARTESIAN_POINT ( 'NONE',  ( 22.63393739769619728, -15.61618894467929941, -5.690000000000000391 ) ) ;
#45966=VECTOR ( 'NONE', #4371, 1000.000000000000000 ) ;
#45978=EDGE_CURVE ( 'NONE', #5441, #49041, #10795, .T. ) ;
#45994=CONICAL_SURFACE ( 'NONE', #19196, 0.6299999999999977840, 0.7853981633974476129 ) ;
#46002=CARTESIAN_POINT ( 'NONE',  ( 16.13393739769620083, -15.61618894467929941, 9.349999999999999645 ) ) ;
#46016=DIRECTION ( 'NONE',  ( 0.000000000000000000, -1.205285871143275290E-11, -1.000000000000000000 ) ) ;
#46027=EDGE_LOOP ( 'NONE', ( #45238, #28719, #36251, #17923 ) ) ;
#46033=CIRCLE ( 'NONE', #25076, 1.000000000000000888 ) ;
#46052=ORIENTED_EDGE ( 'NONE', *, *, #45058, .T. ) ;
#46054=FACE_OUTER_BOUND ( 'NONE', #31993, .T. ) ;
#46057=FACE_OUTER_BOUND ( 'NONE', #35240, .T. ) ;
#46065=ORIENTED_EDGE ( 'NONE', *, *, #29261, .F. ) ;
#46066=CIRCLE ( 'NONE', #33514, 0.9999999999999940048 ) ;
#46070=CARTESIAN_POINT ( 'NONE',  ( 16.13393739769620083, -15.61618894467929941, -14.03562394879499919 ) ) ;
#46074=DIRECTION ( 'NONE',  ( 0.000000000000000000, 1.000000000000000000, 0.000000000000000000 ) ) ;
#46075=EDGE_CURVE ( 'NONE', #35304, #38311, #44262, .T. ) ;
#46079=DIRECTION ( 'NONE',  ( 0.000000000000000000, -1.000000000000000000, 0.000000000000000000 ) ) ;
#46085=ORIENTED_EDGE ( 'NONE', *, *, #16488, .F. ) ;
#46132=ORIENTED_EDGE ( 'NONE', *, *, #31846, .F. ) ;
#46154=FACE_OUTER_BOUND ( 'NONE', #22150, .T. ) ;
#46171=LINE ( 'NONE', #13676, #13458 ) ;
#46189=DIRECTION ( 'NONE',  ( 0.000000000000000000, 0.000000000000000000, 1.000000000000000000 ) ) ;
#46199=CARTESIAN_POINT ( 'NONE',  ( -22.39277411605874235, 24.23791302157028227, 17.35000000000000142 ) ) ;
#46256=DIRECTION ( 'NONE',  ( -1.000000000000000000, 0.000000000000000000, 0.000000000000000000 ) ) ;
#46262=DIRECTION ( 'NONE',  ( 1.224648637339234427E-16, 1.000000000000000000, -6.470619327693536922E-12 ) ) ;
#46267=CARTESIAN_POINT ( 'NONE',  ( -18.86606260230360022, -50.61618894467959962, 16.21999999999999886 ) ) ;
#46272=EDGE_CURVE ( 'NONE', #727, #16578, #40889, .T. ) ;
#46283=VERTEX_POINT ( 'NONE', #18954 ) ;
#46294=ADVANCED_FACE ( 'NONE', ( #23130 ), #15029, .T. ) ;
#46313=CIRCLE ( 'NONE', #1103, 5.999999999999998224 ) ;
#46351=ORIENTED_EDGE ( 'NONE', *, *, #14117, .T. ) ;
#46355=AXIS2_PLACEMENT_3D ( 'NONE', #24302, #51605, #31654 ) ;
#46361=ORIENTED_EDGE ( 'NONE', *, *, #268, .T. ) ;
#46380=ORIENTED_EDGE ( 'NONE', *, *, #8618, .F. ) ;
#46388=CIRCLE ( 'NONE', #48029, 10.00000000000000711 ) ;
#46407=CARTESIAN_POINT ( 'NONE',  ( 16.13393739769620083, -15.61618894467929941, -18.35000000000000142 ) ) ;
#46430=CARTESIAN_POINT ( 'NONE',  ( 47.60722588394173727, -45.76208697842935891, 17.35000000000000142 ) ) ;
#46462=CARTESIAN_POINT ( 'NONE',  ( -18.86606260230390220, 19.38381105532060289, 10.84999999999999964 ) ) ;
#46470=CYLINDRICAL_SURFACE ( 'NONE', #50180, 5.499999999999998224 ) ;
#46472=AXIS2_PLACEMENT_3D ( 'NONE', #507, #48475, #23306 ) ;
#46506=CONICAL_SURFACE ( 'NONE', #37273, 0.6299999999999942313, 0.7853981633974476129 ) ;
#46537=ORIENTED_EDGE ( 'NONE', *, *, #30428, .F. ) ;
#46542=VECTOR ( 'NONE', #49215, 1000.000000000000114 ) ;
#46554=CARTESIAN_POINT ( 'NONE',  ( 16.13393739769620083, -15.61618894467929941, -18.35000000000000142 ) ) ;
#46577=DIRECTION ( 'NONE',  ( 1.000000000000000000, 0.000000000000000000, 0.000000000000000000 ) ) ;
#46582=CIRCLE ( 'NONE', #38231, 3.569999999987189199 ) ;
#46591=FACE_OUTER_BOUND ( 'NONE', #48329, .T. ) ;
#46600=DIRECTION ( 'NONE',  ( 1.000000000000000000, 0.000000000000000000, 0.000000000000000000 ) ) ;
#46606=CARTESIAN_POINT ( 'NONE',  ( 16.13393739769620083, -15.61618894467929941, -19.83999999999999986 ) ) ;
#46617=ORIENTED_EDGE ( 'NONE', *, *, #32368, .T. ) ;
#46633=AXIS2_PLACEMENT_3D ( 'NONE', #13196, #36746, #36487 ) ;
#46636=EDGE_CURVE ( 'NONE', #33390, #727, #23321, .T. ) ;
#46649=FACE_OUTER_BOUND ( 'NONE', #17116, .T. ) ;
#46675=ADVANCED_FACE ( 'NONE', ( #3563 ), #2444, .F. ) ;
#46681=DIRECTION ( 'NONE',  ( -2.619602780254359830E-11, 3.858400438143729530E-12, 1.000000000000000000 ) ) ;
#46689=FACE_BOUND ( 'NONE', #2252, .T. ) ;
#46718=DIRECTION ( 'NONE',  ( 0.000000000000000000, 0.000000000000000000, -1.000000000000000000 ) ) ;
#46730=CARTESIAN_POINT ( 'NONE',  ( 51.13393739769620083, 19.38381105532069881, 14.21249999999999858 ) ) ;
#46744=ORIENTED_EDGE ( 'NONE', *, *, #14254, .F. ) ;
#46750=CARTESIAN_POINT ( 'NONE',  ( 16.13393739769620083, -15.61618894467929941, -18.58999999999999986 ) ) ;
#46766=CIRCLE ( 'NONE', #35843, 12.50000000000000000 ) ;
#46783=CARTESIAN_POINT ( 'NONE',  ( 39.88393739769619373, 30.88381105532059934, 16.35000000000000142 ) ) ;
#46816=ORIENTED_EDGE ( 'NONE', *, *, #22325, .F. ) ;
#46825=DIRECTION ( 'NONE',  ( -1.000000000000000000, 0.000000000000000000, 0.000000000000000000 ) ) ;
#46835=PRODUCT_DEFINITION_CONTEXT ( 'detailed design', #35476, 'design' ) ;
#46853=DIRECTION ( 'NONE',  ( 0.000000000000000000, 0.000000000000000000, 1.000000000000000000 ) ) ;
#46863=VERTEX_POINT ( 'NONE', #49401 ) ;
#46867=AXIS2_PLACEMENT_3D ( 'NONE', #39526, #42947, #7044 ) ;
#46868=CYLINDRICAL_SURFACE ( 'NONE', #40299, 11.00000000000000000 ) ;
#46889=DIRECTION ( 'NONE',  ( 1.000000000000000000, 0.000000000000000000, 0.000000000000000000 ) ) ;
#46899=CARTESIAN_POINT ( 'NONE',  ( 53.63393739769619373, 21.88381105532059934, 10.84999999999999964 ) ) ;
#46911=VERTEX_POINT ( 'NONE', #647 ) ;
#46915=CARTESIAN_POINT ( 'NONE',  ( 46.27983543144652856, 15.85709954156585155, 17.35000000000000142 ) ) ;
#46945=ORIENTED_EDGE ( 'NONE', *, *, #47389, .F. ) ;
#46955=CARTESIAN_POINT ( 'NONE',  ( -30.36606260230379917, -15.61618894467929941, 11.84999999999999964 ) ) ;
#46965=LINE ( 'NONE', #39595, #37640 ) ;
#46985=CIRCLE ( 'NONE', #41126, 13.50000000000000000 ) ;
#47000=EDGE_CURVE ( 'NONE', #17463, #31353, #49334, .T. ) ;
#47018=DIRECTION ( 'NONE',  ( 0.000000000000000000, 0.000000000000000000, 1.000000000000000000 ) ) ;
#47021=AXIS2_PLACEMENT_3D ( 'NONE', #20698, #5002, #5526 ) ;
#47050=ADVANCED_FACE ( 'NONE', ( #2460 ), #27574, .F. ) ;
#47054=ORIENTED_EDGE ( 'NONE', *, *, #4554, .F. ) ;
#47055=LINE ( 'NONE', #3794, #20876 ) ;
#47071=ORIENTED_EDGE ( 'NONE', *, *, #6028, .F. ) ;
#47072=ORIENTED_EDGE ( 'NONE', *, *, #3770, .T. ) ;
#47080=DIRECTION ( 'NONE',  ( 0.000000000000000000, 0.000000000000000000, 1.000000000000000000 ) ) ;
#47099=CARTESIAN_POINT ( 'NONE',  ( 55.98803936394586600, 22.91052256907554963, 17.35000000000000142 ) ) ;
#47112=DIRECTION ( 'NONE',  ( 0.000000000000000000, 0.000000000000000000, 1.000000000000000000 ) ) ;
#47122=CARTESIAN_POINT ( 'NONE',  ( 53.63393739769619373, -62.82329572586585442, 17.05710678118654400 ) ) ;
#47124=AXIS2_PLACEMENT_3D ( 'NONE', #48934, #37379, #13035 ) ;
#47132=CARTESIAN_POINT ( 'NONE',  ( 24.22410734144567357, -9.738336421754578254, -5.966499999999999915 ) ) ;
#47157=AXIS2_PLACEMENT_3D ( 'NONE', #36918, #45825, #17017 ) ;
#47159=DIRECTION ( 'NONE',  ( 0.000000000000000000, 0.000000000000000000, -1.000000000000000000 ) ) ;
#47169=ORIENTED_EDGE ( 'NONE', *, *, #30493, .T. ) ;
#47191=VERTEX_POINT ( 'NONE', #43847 ) ;
#47199=CIRCLE ( 'NONE', #38816, 1.000000000000000888 ) ;
#47201=CIRCLE ( 'NONE', #47157, 5.499999999999998224 ) ;
#47207=FACE_OUTER_BOUND ( 'NONE', #22595, .T. ) ;
#47216=TOROIDAL_SURFACE ( 'NONE', #25393, 19.50000000000000000, 0.5000000000000000000 ) ;
#47230=ORIENTED_EDGE ( 'NONE', *, *, #836, .F. ) ;
#47239=DIRECTION ( 'NONE',  ( 0.000000000000000000, 0.000000000000000000, -1.000000000000000000 ) ) ;
#47254=VERTEX_POINT ( 'NONE', #11113 ) ;
#47255=AXIS2_PLACEMENT_3D ( 'NONE', #33635, #25504, #5623 ) ;
#47289=CIRCLE ( 'NONE', #24646, 5.499999999999998224 ) ;
#47294=DIRECTION ( 'NONE',  ( 0.000000000000000000, 1.000000000000000000, 0.000000000000000000 ) ) ;
#47296=EDGE_CURVE ( 'NONE', #44094, #26084, #44339, .T. ) ;
#47318=ORIENTED_EDGE ( 'NONE', *, *, #51590, .T. ) ;
#47325=ORIENTED_EDGE ( 'NONE', *, *, #20093, .F. ) ;
#47326=CARTESIAN_POINT ( 'NONE',  ( 6.133937397696199945, -15.61618894467930119, 17.35000000000000142 ) ) ;
#47330=CARTESIAN_POINT ( 'NONE',  ( 16.13393739769620083, -15.61618894467929941, -14.68999999999999950 ) ) ;
#47340=DIRECTION ( 'NONE',  ( 0.000000000000000000, 0.000000000000000000, -1.000000000000000000 ) ) ;
#47355=CARTESIAN_POINT ( 'NONE',  ( 63.63393739769619373, -53.11618894467930119, 11.84999999999999964 ) ) ;
#47377=AXIS2_PLACEMENT_3D ( 'NONE', #11788, #5470, #29040 ) ;
#47380=ORIENTED_EDGE ( 'NONE', *, *, #18309, .F. ) ;
#47382=VECTOR ( 'NONE', #41995, 1000.000000000000114 ) ;
#47389=EDGE_CURVE ( 'NONE', #11901, #18483, #40152, .T. ) ;
#47396=AXIS2_PLACEMENT_3D ( 'NONE', #4403, #35858, #20894 ) ;
#47427=CIRCLE ( 'NONE', #28997, 5.999999999999998224 ) ;
#47457=CONICAL_SURFACE ( 'NONE', #25641, 0.6299999999999866818, 0.7853981633974476129 ) ;
#47458=CARTESIAN_POINT ( 'NONE',  ( 16.13393739769620083, -15.61618894467929941, -9.392532499999980189 ) ) ;
#47468=DIRECTION ( 'NONE',  ( 0.8090169943749473402, 0.5877852522924732481, 0.000000000000000000 ) ) ;
#47470=EDGE_CURVE ( 'NONE', #19682, #35239, #23395, .T. ) ;
#47472=ADVANCED_FACE ( 'NONE', ( #43024 ), #39091, .T. ) ;
#47483=ORIENTED_EDGE ( 'NONE', *, *, #36763, .F. ) ;
#47505=VERTEX_POINT ( 'NONE', #23317 ) ;
#47513=DIRECTION ( 'NONE',  ( -1.000000000000000000, 0.000000000000000000, 0.000000000000000000 ) ) ;
#47531=TOROIDAL_SURFACE ( 'NONE', #2330, 19.50000000000000000, 0.5000000000000000000 ) ;
#47539=DIRECTION ( 'NONE',  ( 0.000000000000000000, 0.000000000000000000, 1.000000000000000000 ) ) ;
#47541=ORIENTED_EDGE ( 'NONE', *, *, #31307, .F. ) ;
#47559=ORIENTED_EDGE ( 'NONE', *, *, #22027, .F. ) ;
#47575=EDGE_CURVE ( 'NONE', #4191, #27635, #46965, .T. ) ;
#47577=EDGE_CURVE ( 'NONE', #34457, #29477, #20036, .T. ) ;
#47605=DIRECTION ( 'NONE',  ( -1.000000000000000000, 0.000000000000000000, 0.000000000000000000 ) ) ;
#47625=FACE_OUTER_BOUND ( 'NONE', #17137, .T. ) ;
#47629=ADVANCED_FACE ( 'NONE', ( #8139 ), #17039, .F. ) ;
#47637=CARTESIAN_POINT ( 'NONE',  ( 16.13393739769620083, -15.61618894467929941, -2.149999999999999911 ) ) ;
#47648=DIRECTION ( 'NONE',  ( 0.000000000000000000, 0.000000000000000000, 1.000000000000000000 ) ) ;
#47658=CARTESIAN_POINT ( 'NONE',  ( 11.19893373200904740, -19.20167898366336345, -8.849999999999999645 ) ) ;
#47669=DIRECTION ( 'NONE',  ( 0.000000000000000000, 0.000000000000000000, 1.000000000000000000 ) ) ;
#47684=CYLINDRICAL_SURFACE ( 'NONE', #47377, 10.00000000000000711 ) ;
#47687=EDGE_LOOP ( 'NONE', ( #26596, #29984 ) ) ;
#47700=ORIENTED_EDGE ( 'NONE', *, *, #19416, .F. ) ;
#47706=DIRECTION ( 'NONE',  ( 0.7071067811865475727, -0.7071067811865475727, 0.000000000000000000 ) ) ;
#47722=DIRECTION ( 'NONE',  ( 0.000000000000000000, 0.000000000000000000, 1.000000000000000000 ) ) ;
#47733=CARTESIAN_POINT ( 'NONE',  ( -30.36606260230379917, -53.11618894467930119, 11.84999999999999964 ) ) ;
#47746=CYLINDRICAL_SURFACE ( 'NONE', #7084, 0.9999999999999988898 ) ;
#47750=TOROIDAL_SURFACE ( 'NONE', #36848, 9.000000000000000000, 1.000000000000000000 ) ;
#47757=FACE_OUTER_BOUND ( 'NONE', #15391, .T. ) ;
#47762=DIRECTION ( 'NONE',  ( 0.000000000000000000, 1.377023495004005809E-11, 1.000000000000000000 ) ) ;
#47819=VERTEX_POINT ( 'NONE', #8485 ) ;
#47837=CARTESIAN_POINT ( 'NONE',  ( -31.07316938349034885, -15.61618894467929941, 11.14289321881345174 ) ) ;
#47862=CARTESIAN_POINT ( 'NONE',  ( -18.86606260230360022, -50.61618894467959962, 16.85000000000000142 ) ) ;
#47865=ORIENTED_EDGE ( 'NONE', *, *, #10833, .F. ) ;
#47872=DIRECTION ( 'NONE',  ( 0.5877852522924733591, -0.8090169943749473402, 0.000000000000000000 ) ) ;
#47875=CARTESIAN_POINT ( 'NONE',  ( 63.34104417888273986, -53.11618894467930119, 17.05710678118654755 ) ) ;
#47879=EDGE_LOOP ( 'NONE', ( #51742, #8503, #11802, #16205, #46052 ) ) ;
#47896=FACE_OUTER_BOUND ( 'NONE', #42279, .T. ) ;
#47924=DIRECTION ( 'NONE',  ( 1.000000000000000000, 0.000000000000000000, 0.000000000000000000 ) ) ;
#47935=CARTESIAN_POINT ( 'NONE',  ( 16.13393739769620083, -15.61618894467929941, -20.58999999999999986 ) ) ;
#47940=CARTESIAN_POINT ( 'NONE',  ( 53.63393739769619373, -62.11618894467930119, 16.35000000000000142 ) ) ;
#47944=EDGE_LOOP ( 'NONE', ( #35034, #35063, #33036, #42194 ) ) ;
#47983=AXIS2_PLACEMENT_3D ( 'NONE', #3655, #31913, #39805 ) ;
#48021=VERTEX_POINT ( 'NONE', #47875 ) ;
#48029=AXIS2_PLACEMENT_3D ( 'NONE', #45050, #41627, #20664 ) ;
#48030=DIRECTION ( 'NONE',  ( 1.000000000000000000, 0.000000000000000000, 0.000000000000000000 ) ) ;
#48034=ORIENTED_EDGE ( 'NONE', *, *, #30165, .F. ) ;
#48067=DIRECTION ( 'NONE',  ( 0.000000000000000000, 0.000000000000000000, -1.000000000000000000 ) ) ;
#48070=FACE_OUTER_BOUND ( 'NONE', #28615, .T. ) ;
#48076=AXIS2_PLACEMENT_3D ( 'NONE', #41424, #26200, #37243 ) ;
#48089=DIRECTION ( 'NONE',  ( -1.000000000000000000, 0.000000000000000000, 0.000000000000000000 ) ) ;
#48099=EDGE_CURVE ( 'NONE', #13493, #45507, #7572, .T. ) ;
#48118=ORIENTED_EDGE ( 'NONE', *, *, #22207, .F. ) ;
#48144=CARTESIAN_POINT ( 'NONE',  ( -18.86606260230390220, 19.38381105532060289, 14.21249999999999858 ) ) ;
#48147=DIRECTION ( 'NONE',  ( -1.000000000000000000, 0.000000000000000000, 0.000000000000000000 ) ) ;
#48157=FACE_OUTER_BOUND ( 'NONE', #22704, .T. ) ;
#48162=AXIS2_PLACEMENT_3D ( 'NONE', #15739, #44284, #11563 ) ;
#48165=EDGE_CURVE ( 'NONE', #6375, #51520, #12583, .T. ) ;
#48194=DIRECTION ( 'NONE',  ( 0.000000000000000000, 1.000000000000000000, 0.000000000000000000 ) ) ;
#48226=DIRECTION ( 'NONE',  ( 0.000000000000000000, 0.000000000000000000, 1.000000000000000000 ) ) ;
#48227=AXIS2_PLACEMENT_3D ( 'NONE', #18853, #42466, #6301 ) ;
#48243=ORIENTED_EDGE ( 'NONE', *, *, #2657, .T. ) ;
#48245=EDGE_CURVE ( 'NONE', #25374, #6898, #30103, .T. ) ;
#48264=VECTOR ( 'NONE', #11900, 1000.000000000000000 ) ;
#48268=VERTEX_POINT ( 'NONE', #45233 ) ;
#48274=CARTESIAN_POINT ( 'NONE',  ( 51.13393739769659874, -45.11618894467899565, 11.34999999999999964 ) ) ;
#48282=CIRCLE ( 'NONE', #9793, 36.50000000000000711 ) ;
#48285=( NAMED_UNIT ( * ) PLANE_ANGLE_UNIT ( ) SI_UNIT ( $, .RADIAN. ) );
#48293=AXIS2_PLACEMENT_3D ( 'NONE', #37282, #24678, #40691 ) ;
#48299=DIRECTION ( 'NONE',  ( 0.000000000000000000, 0.000000000000000000, -1.000000000000000000 ) ) ;
#48321=CYLINDRICAL_SURFACE ( 'NONE', #10723, 5.499999999999998224 ) ;
#48329=EDGE_LOOP ( 'NONE', ( #46617, #16561, #8124, #16473, #7289 ) ) ;
#48343=CARTESIAN_POINT ( 'NONE',  ( 16.13393739769620083, -15.61618894467929941, -18.58999999999999986 ) ) ;
#48387=ORIENTED_EDGE ( 'NONE', *, *, #29261, .T. ) ;
#48398=CARTESIAN_POINT ( 'NONE',  ( 10.03393739769619941, -15.61618894467929941, 14.34999999999999964 ) ) ;
#48410=CARTESIAN_POINT ( 'NONE',  ( -18.86606260230360022, -50.61618894467959962, 17.35000000000000142 ) ) ;
#48417=AXIS2_PLACEMENT_3D ( 'NONE', #8308, #24521, #24265 ) ;
#48435=DIRECTION ( 'NONE',  ( 0.000000000000000000, -1.377023495004005809E-11, -1.000000000000000000 ) ) ;
#48456=DIRECTION ( 'NONE',  ( 1.000000000000000000, 0.000000000000000000, 0.000000000000000000 ) ) ;
#48461=CARTESIAN_POINT ( 'NONE',  ( 29.63393739769620083, -15.61618894467929941, -11.11999999999999922 ) ) ;
#48471=DIRECTION ( 'NONE',  ( 0.8090169943749525583, 0.5877852522924661427, 0.000000000000000000 ) ) ;
#48475=DIRECTION ( 'NONE',  ( 0.000000000000000000, 0.000000000000000000, 1.000000000000000000 ) ) ;
#48505=ADVANCED_FACE ( 'NONE', ( #5087 ), #27603, .T. ) ;
#48526=ORIENTED_EDGE ( 'NONE', *, *, #22325, .T. ) ;
#48531=CIRCLE ( 'NONE', #25904, 5.999999999999998224 ) ;
#48532=ORIENTED_EDGE ( 'NONE', *, *, #32623, .T. ) ;
#48534=AXIS2_PLACEMENT_3D ( 'NONE', #49910, #17676, #6145 ) ;
#48539=DIRECTION ( 'NONE',  ( 0.000000000000000000, 0.000000000000000000, 1.000000000000000000 ) ) ;
#48540=VECTOR ( 'NONE', #30650, 1000.000000000000000 ) ;
#48560=VECTOR ( 'NONE', #13490, 1000.000000000000114 ) ;
#48563=CIRCLE ( 'NONE', #50250, 0.5000000000000004441 ) ;
#48566=AXIS2_PLACEMENT_3D ( 'NONE', #39749, #36310, #27933 ) ;
#48589=CARTESIAN_POINT ( 'NONE',  ( -21.36606260230379917, -53.11618894467930119, 16.35000000000000142 ) ) ;
#48590=ORIENTED_EDGE ( 'NONE', *, *, #29319, .T. ) ;
#48609=CARTESIAN_POINT ( 'NONE',  ( -18.86606260230390220, 19.38381105532060289, 11.34999999999999964 ) ) ;
#48614=VECTOR ( 'NONE', #45835, 1000.000000000000000 ) ;
#48643=AXIS2_PLACEMENT_3D ( 'NONE', #33566, #41964, #1866 ) ;
#48680=ADVANCED_FACE ( 'NONE', ( #47757 ), #20083, .F. ) ;
#48684=TOROIDAL_SURFACE ( 'NONE', #33192, 9.000000000000000000, 1.000000000000000000 ) ;
#48686=DIRECTION ( 'NONE',  ( 0.7071067811865475727, -0.7071067811865475727, 0.000000000000000000 ) ) ;
#48687=AXIS2_PLACEMENT_3D ( 'NONE', #17976, #33688, #33942 ) ;
#48816=ORIENTED_EDGE ( 'NONE', *, *, #6734, .T. ) ;
#48825=CIRCLE ( 'NONE', #22050, 20.00000000000000000 ) ;
#48842=FACE_OUTER_BOUND ( 'NONE', #30631, .T. ) ;
#48870=VECTOR ( 'NONE', #18840, 1000.000000000000114 ) ;
#48874=AXIS2_PLACEMENT_3D ( 'NONE', #42607, #15339, #38681 ) ;
#48905=ORIENTED_EDGE ( 'NONE', *, *, #6688, .T. ) ;
#48919=CARTESIAN_POINT ( 'NONE',  ( -21.36606260230379917, -53.11618894467930119, 16.35000000000000142 ) ) ;
#48934=CARTESIAN_POINT ( 'NONE',  ( 16.13393739769620083, -15.61618894467929941, 14.62639320225000006 ) ) ;
#48937=CYLINDRICAL_SURFACE ( 'NONE', #19227, 5.499999999999998224 ) ;
#48964=CIRCLE ( 'NONE', #46472, 9.000000000000007105 ) ;
#48968=CARTESIAN_POINT ( 'NONE',  ( -30.36606260230379917, 21.88381105532059934, 16.35000000000000142 ) ) ;
#48998=DIRECTION ( 'NONE',  ( -1.000000000000000000, 0.000000000000000000, 0.000000000000000000 ) ) ;
#49000=FACE_OUTER_BOUND ( 'NONE', #42384, .T. ) ;
#49001=FACE_OUTER_BOUND ( 'NONE', #21213, .T. ) ;
#49009=DIRECTION ( 'NONE',  ( 0.000000000000000000, 0.000000000000000000, -1.000000000000000000 ) ) ;
#49016=DIRECTION ( 'NONE',  ( -1.000000000000000000, 0.000000000000000000, 0.000000000000000000 ) ) ;
#49021=CARTESIAN_POINT ( 'NONE',  ( 16.13393739769620083, -15.61618894467929941, -1.149999999999999911 ) ) ;
#49031=DIRECTION ( 'NONE',  ( 1.000000000000000000, 0.000000000000000000, 0.000000000000000000 ) ) ;
#49041=VERTEX_POINT ( 'NONE', #18609 ) ;
#49058=AXIS2_PLACEMENT_3D ( 'NONE', #43405, #19030, #28166 ) ;
#49066=FACE_OUTER_BOUND ( 'NONE', #43163, .T. ) ;
#49067=AXIS2_PLACEMENT_3D ( 'NONE', #36737, #44613, #41455 ) ;
#49099=LINE ( 'NONE', #21541, #37074 ) ;
#49131=VERTEX_POINT ( 'NONE', #1472 ) ;
#49161=LINE ( 'NONE', #41535, #41506 ) ;
#49168=ADVANCED_FACE ( 'NONE', ( #33162 ), #36024, .T. ) ;
#49186=CARTESIAN_POINT ( 'NONE',  ( 16.13393739769620083, -15.61618894467929941, -18.58999999999999986 ) ) ;
#49215=DIRECTION ( 'NONE',  ( -0.5720614028176831400, 0.4156269377774557960, -0.7071067811865470176 ) ) ;
#49239=DIRECTION ( 'NONE',  ( -1.000000000000000000, 0.000000000000000000, 0.000000000000000000 ) ) ;
#49241=ORIENTED_EDGE ( 'NONE', *, *, #14775, .T. ) ;
#49257=DIRECTION ( 'NONE',  ( 0.000000000000000000, -1.000000000000000000, 0.000000000000000000 ) ) ;
#49274=ORIENTED_EDGE ( 'NONE', *, *, #23679, .T. ) ;
#49295=AXIS2_PLACEMENT_3D ( 'NONE', #13854, #50534, #10702 ) ;
#49327=CARTESIAN_POINT ( 'NONE',  ( 45.63393739769620083, 19.38381105532069881, 14.21249999999999858 ) ) ;
#49334=CIRCLE ( 'NONE', #21683, 6.100000000000001421 ) ;
#49345=ORIENTED_EDGE ( 'NONE', *, *, #11704, .F. ) ;
#49351=ORIENTED_EDGE ( 'NONE', *, *, #36763, .T. ) ;
#49356=DIRECTION ( 'NONE',  ( 0.000000000000000000, 0.000000000000000000, 1.000000000000000000 ) ) ;
#49359=CARTESIAN_POINT ( 'NONE',  ( 16.13393739769620083, -15.61618894467929941, -14.88746750000000141 ) ) ;
#49368=CARTESIAN_POINT ( 'NONE',  ( 34.41893739769619742, -15.61618894467929941, -14.68999999999999950 ) ) ;
#49374=AXIS2_PLACEMENT_3D ( 'NONE', #20174, #19917, #24347 ) ;
#49390=ORIENTED_EDGE ( 'NONE', *, *, #15013, .T. ) ;
#49393=CARTESIAN_POINT ( 'NONE',  ( -19.37574330875981587, -50.98649365362385311, 11.97999999999999865 ) ) ;
#49394=ORIENTED_EDGE ( 'NONE', *, *, #35831, .T. ) ;
#49395=DIRECTION ( 'NONE',  ( 0.000000000000000000, 0.000000000000000000, 1.000000000000000000 ) ) ;
#49401=CARTESIAN_POINT ( 'NONE',  ( 60.70500520956166923, 28.95487886718607484, 11.84999999999999964 ) ) ;
#49424=ORIENTED_EDGE ( 'NONE', *, *, #39185, .T. ) ;
#49430=DIRECTION ( 'NONE',  ( 0.000000000000000000, -1.000000000000000000, 0.000000000000000000 ) ) ;
#49433=DIRECTION ( 'NONE',  ( 0.000000000000000000, 0.000000000000000000, 1.000000000000000000 ) ) ;
#49436=VERTEX_POINT ( 'NONE', #4052 ) ;
#49442=TOROIDAL_SURFACE ( 'NONE', #27641, 18.49999999936520112, 4.999999999969890752 ) ;
#49446=CIRCLE ( 'NONE', #7573, 5.499999999999998224 ) ;
#49454=ORIENTED_EDGE ( 'NONE', *, *, #39280, .T. ) ;
#49474=CARTESIAN_POINT ( 'NONE',  ( 53.63393739769619373, 31.59091783650714547, 17.05710678118654755 ) ) ;
#49483=DIRECTION ( 'NONE',  ( 1.000000000000000000, 0.000000000000000000, 0.000000000000000000 ) ) ;
#49505=ORIENTED_EDGE ( 'NONE', *, *, #6082, .T. ) ;
#49511=DIRECTION ( 'NONE',  ( 0.000000000000000000, -1.000000000000000000, 0.000000000000000000 ) ) ;
#49517=VERTEX_POINT ( 'NONE', #41400 ) ;
#49525=VERTEX_POINT ( 'NONE', #37995 ) ;
#49548=ORIENTED_EDGE ( 'NONE', *, *, #7702, .T. ) ;
#49578=ORIENTED_EDGE ( 'NONE', *, *, #29395, .T. ) ;
#49586=DIRECTION ( 'NONE',  ( 1.000000000000000000, 0.000000000000000000, 0.000000000000000000 ) ) ;
#49623=DIRECTION ( 'NONE',  ( 0.000000000000000000, 0.000000000000000000, -1.000000000000000000 ) ) ;
#49636=EDGE_LOOP ( 'NONE', ( #1405, #26079 ) ) ;
#49698=AXIS2_PLACEMENT_3D ( 'NONE', #22184, #1773, #14601 ) ;
#49701=CONICAL_SURFACE ( 'NONE', #14562, 0.6299999999999977840, 0.7853981633974476129 ) ;
#49703=EDGE_LOOP ( 'NONE', ( #45098, #12392, #22664, #15976 ) ) ;
#49727=DIRECTION ( 'NONE',  ( 0.000000000000000000, 0.000000000000000000, -1.000000000000000000 ) ) ;
#49748=AXIS2_PLACEMENT_3D ( 'NONE', #12643, #40158, #48030 ) ;
#49750=EDGE_CURVE ( 'NONE', #10341, #44765, #20034, .T. ) ;
#49759=DIRECTION ( 'NONE',  ( 0.000000000000000000, 0.000000000000000000, 1.000000000000000000 ) ) ;
#49760=CIRCLE ( 'NONE', #16262, 3.569999999987189199 ) ;
#49789=FACE_OUTER_BOUND ( 'NONE', #41728, .T. ) ;
#49819=ADVANCED_FACE ( 'NONE', ( #16457, #32412 ), #21658, .T. ) ;
#49854=AXIS2_PLACEMENT_3D ( 'NONE', #20426, #40105, #36413 ) ;
#49864=ORIENTED_EDGE ( 'NONE', *, *, #11648, .T. ) ;
#49873=CYLINDRICAL_SURFACE ( 'NONE', #34188, 10.00000000000000355 ) ;
#49889=CARTESIAN_POINT ( 'NONE',  ( 16.65211278259335614, -15.23971249058597088, -12.13039854958090125 ) ) ;
#49904=ORIENTED_EDGE ( 'NONE', *, *, #27404, .T. ) ;
#49910=CARTESIAN_POINT ( 'NONE',  ( 51.13393739769659874, -50.61618894467899565, 11.97999999999999865 ) ) ;
#49913=EDGE_CURVE ( 'NONE', #40580, #44712, #43596, .T. ) ;
#49915=VERTEX_POINT ( 'NONE', #12803 ) ;
#49923=EDGE_CURVE ( 'NONE', #42477, #25606, #21151, .T. ) ;
#49934=ORIENTED_EDGE ( 'NONE', *, *, #18249, .F. ) ;
#49965=CONICAL_SURFACE ( 'NONE', #18158, 1.079032500000002059, 0.7853981633974469467 ) ;
#49980=CARTESIAN_POINT ( 'NONE',  ( 53.63393739769619373, 21.88381105532059934, 11.84999999999999964 ) ) ;
#49991=CARTESIAN_POINT ( 'NONE',  ( 16.13393739769620083, -15.61618894467929941, -20.58999999999999986 ) ) ;
#50002=CARTESIAN_POINT ( 'NONE',  ( 62.63393739769619373, -53.11618894467930119, 10.84999999999999964 ) ) ;
#50005=VERTEX_POINT ( 'NONE', #47355 ) ;
#50020=DIRECTION ( 'NONE',  ( 1.000000000000000000, 0.000000000000000000, 0.000000000000000000 ) ) ;
#50028=VERTEX_POINT ( 'NONE', #39734 ) ;
#50052=VERTEX_POINT ( 'NONE', #31583 ) ;
#50085=DIRECTION ( 'NONE',  ( -0.7071067811865475727, 0.7071067811865475727, 0.000000000000000000 ) ) ;
#50099=EDGE_CURVE ( 'NONE', #50028, #44136, #33434, .T. ) ;
#50105=EDGE_CURVE ( 'NONE', #7343, #49436, #24204, .T. ) ;
#50108=ORIENTED_EDGE ( 'NONE', *, *, #36196, .F. ) ;
#50112=DIRECTION ( 'NONE',  ( -0.7071067811865476838, -0.7071067811865473507, 0.000000000000000000 ) ) ;
#50118=DIRECTION ( 'NONE',  ( 0.000000000000000000, 1.000000000000000000, 0.000000000000000000 ) ) ;
#50153=ORIENTED_EDGE ( 'NONE', *, *, #28621, .T. ) ;
#50155=DIRECTION ( 'NONE',  ( 0.000000000000000000, 1.000000000000000000, 0.000000000000000000 ) ) ;
#50164=EDGE_CURVE ( 'NONE', #19246, #20846, #34369, .T. ) ;
#50172=LINE ( 'NONE', #10081, #41399 ) ;
#50177=AXIS2_PLACEMENT_3D ( 'NONE', #24034, #43731, #20373 ) ;
#50180=AXIS2_PLACEMENT_3D ( 'NONE', #46730, #22582, #34114 ) ;
#50187=DIRECTION ( 'NONE',  ( 0.000000000000000000, 0.000000000000000000, -1.000000000000000000 ) ) ;
#50195=EDGE_LOOP ( 'NONE', ( #13136, #7475 ) ) ;
#50206=EDGE_LOOP ( 'NONE', ( #37665, #11351, #11214, #7003 ) ) ;
#50215=CARTESIAN_POINT ( 'NONE',  ( 51.13393739769659874, -50.61618894467899565, 10.84999999999999964 ) ) ;
#50237=SURFACE_SIDE_STYLE ('',( #38179 ) ) ;
#50240=DIRECTION ( 'NONE',  ( 0.000000000000000000, 0.7071067811865457964, 0.7071067811865492381 ) ) ;
#50249=VERTEX_POINT ( 'NONE', #5900 ) ;
#50250=AXIS2_PLACEMENT_3D ( 'NONE', #43820, #7669, #7918 ) ;
#50252=EDGE_LOOP ( 'NONE', ( #2534, #36578, #45823, #13519, #3480 ) ) ;
#50267=DIRECTION ( 'NONE',  ( -1.000000000000000000, 0.000000000000000000, 0.000000000000000000 ) ) ;
#50276=ORIENTED_EDGE ( 'NONE', *, *, #47000, .T. ) ;
#50298=AXIS2_PLACEMENT_3D ( 'NONE', #7513, #43922, #47605 ) ;
#50318=ORIENTED_EDGE ( 'NONE', *, *, #23858, .T. ) ;
#50330=CARTESIAN_POINT ( 'NONE',  ( 62.63393739769619373, 21.88381105532059934, 17.35000000000000142 ) ) ;
#50352=DIRECTION ( 'NONE',  ( 0.000000000000000000, 0.000000000000000000, 1.000000000000000000 ) ) ;
#50353=DIRECTION ( 'NONE',  ( 0.000000000000000000, 1.000000000000000000, 0.000000000000000000 ) ) ;
#50370=AXIS2_PLACEMENT_3D ( 'NONE', #19701, #4484, #31473 ) ;
#50390=FACE_OUTER_BOUND ( 'NONE', #21512, .T. ) ;
#50410=CARTESIAN_POINT ( 'NONE',  ( 53.63393739769619373, 21.88381105532059934, 17.35000000000000142 ) ) ;
#50411=CIRCLE ( 'NONE', #11095, 9.999999999999998224 ) ;
#50414=VERTEX_POINT ( 'NONE', #17992 ) ;
#50461=CARTESIAN_POINT ( 'NONE',  ( 63.63393739769619373, 21.88381105532059934, 11.84999999999999964 ) ) ;
#50471=EDGE_LOOP ( 'NONE', ( #20912, #43829, #19814, #23540, #24339 ) ) ;
#50528=ORIENTED_EDGE ( 'NONE', *, *, #34515, .F. ) ;
#50534=DIRECTION ( 'NONE',  ( -1.000000000000000000, 0.000000000000000000, 0.000000000000000000 ) ) ;
#50549=CIRCLE ( 'NONE', #7867, 5.500000000000000000 ) ;
#50552=CARTESIAN_POINT ( 'NONE',  ( 45.63393739769620083, 19.38381105532069881, 11.34999999999999964 ) ) ;
#50559=EDGE_CURVE ( 'NONE', #4500, #44239, #7534, .T. ) ;
#50565=CARTESIAN_POINT ( 'NONE',  ( 16.13393739954389972, -15.61618894518879941, 4.350000000321379900 ) ) ;
#50569=EDGE_CURVE ( 'NONE', #32442, #35847, #35124, .T. ) ;
#50596=ORIENTED_EDGE ( 'NONE', *, *, #22003, .T. ) ;
#50616=MECHANICAL_DESIGN_GEOMETRIC_PRESENTATION_REPRESENTATION('',(#7936),#36377);
#50653=CARTESIAN_POINT ( 'NONE',  ( 53.63393739769619373, -62.11618894467930119, 16.35000000000000142 ) ) ;
#50685=EDGE_CURVE ( 'NONE', #23063, #20497, #15083, .T. ) ;
#50716=ORIENTED_EDGE ( 'NONE', *, *, #8618, .T. ) ;
#50732=CIRCLE ( 'NONE', #13929, 9.000000000000007105 ) ;
#50733=DIRECTION ( 'NONE',  ( 0.000000000000000000, 0.000000000000000000, 1.000000000000000000 ) ) ;
#50740=DIRECTION ( 'NONE',  ( 0.000000000000000000, 0.000000000000000000, -1.000000000000000000 ) ) ;
#50741=DIRECTION ( 'NONE',  ( 0.000000000000000000, 0.000000000000000000, 1.000000000000000000 ) ) ;
#50748=LINE ( 'NONE', #6732, #34443 ) ;
#50767=CYLINDRICAL_SURFACE ( 'NONE', #19202, 13.50000000000000178 ) ;
#50781=ORIENTED_EDGE ( 'NONE', *, *, #28621, .F. ) ;
#50796=VERTEX_POINT ( 'NONE', #15016 ) ;
#50799=ORIENTED_EDGE ( 'NONE', *, *, #21791, .T. ) ;
#50825=CARTESIAN_POINT ( 'NONE',  ( 50.76363268875235235, -51.12586965113521131, 16.21999999999999886 ) ) ;
#50831=DIRECTION ( 'NONE',  ( 0.000000000000000000, 0.000000000000000000, -1.000000000000000000 ) ) ;
#50838=ORIENTED_EDGE ( 'NONE', *, *, #37197, .T. ) ;
#50849=EDGE_LOOP ( 'NONE', ( #19579, #342, #44151, #29491, #41305, #39951, #17721 ) ) ;
#50878=CARTESIAN_POINT ( 'NONE',  ( 51.13393739769620083, 19.38381105532069881, 16.21999999999999886 ) ) ;
#50892=CIRCLE ( 'NONE', #25768, 5.499999999999998224 ) ;
#50903=CARTESIAN_POINT ( 'NONE',  ( -31.36606260230380272, -53.11618894467930119, 11.84999999999999964 ) ) ;
#50925=ORIENTED_EDGE ( 'NONE', *, *, #33575, .F. ) ;
#50937=DIRECTION ( 'NONE',  ( -0.7071067811865475727, 0.7071067811865475727, 0.000000000000000000 ) ) ;
#50968=CIRCLE ( 'NONE', #45134, 12.50000000000000000 ) ;
#50983=ADVANCED_FACE ( 'NONE', ( #5170 ), #48937, .F. ) ;
#51000=AXIS2_PLACEMENT_3D ( 'NONE', #30761, #38912, #42847 ) ;
#51008=EDGE_CURVE ( 'NONE', #34913, #6962, #41057, .T. ) ;
#51023=CARTESIAN_POINT ( 'NONE',  ( 16.13393739769620083, -15.61618894467929941, -15.18999999999999950 ) ) ;
#51045=DIRECTION ( 'NONE',  ( -1.000000000000000000, 0.000000000000000000, 0.000000000000000000 ) ) ;
#51057=DIRECTION ( 'NONE',  ( 0.000000000000000000, 0.000000000000000000, -1.000000000000000000 ) ) ;
#51067=ORIENTED_EDGE ( 'NONE', *, *, #37132, .F. ) ;
#51075=AXIS2_PLACEMENT_3D ( 'NONE', #27420, #27683, #12224 ) ;
#51087=LINE ( 'NONE', #34830, #42823 ) ;
#51110=VERTEX_POINT ( 'NONE', #26339 ) ;
#51137=CARTESIAN_POINT ( 'NONE',  ( 11.48393739769620048, -15.61618894467929941, -9.721247897589949005 ) ) ;
#51165=DIRECTION ( 'NONE',  ( 0.000000000000000000, 0.000000000000000000, -1.000000000000000000 ) ) ;
#51175=DIRECTION ( 'NONE',  ( 1.430038757655089944E-15, 8.684364315601310195E-16, -1.000000000000000000 ) ) ;
#51184=EDGE_CURVE ( 'NONE', #30215, #14338, #17596, .T. ) ;
#51196=AXIS2_PLACEMENT_3D ( 'NONE', #27418, #36060, #47872 ) ;
#51200=AXIS2_PLACEMENT_3D ( 'NONE', #28289, #44291, #40621 ) ;
#51232=DIRECTION ( 'NONE',  ( 0.000000000000000000, 0.000000000000000000, 1.000000000000000000 ) ) ;
#51233=DIRECTION ( 'NONE',  ( -1.000000000000000000, 0.000000000000000000, 0.000000000000000000 ) ) ;
#51234=ORIENTED_EDGE ( 'NONE', *, *, #31496, .T. ) ;
#51236=TOROIDAL_SURFACE ( 'NONE', #14403, 13.00000000000000000, 0.5000000000000000000 ) ;
#51245=ORIENTED_EDGE ( 'NONE', *, *, #11648, .F. ) ;
#51247=LINE ( 'NONE', #31041, #3531 ) ;
#51262=AXIS2_PLACEMENT_3D ( 'NONE', #13111, #29062, #13610 ) ;
#51272=DIRECTION ( 'NONE',  ( -0.7071067811865475727, 0.7071067811865475727, 0.000000000000000000 ) ) ;
#51280=EDGE_CURVE ( 'NONE', #26468, #21433, #18405, .T. ) ;
#51294=DIRECTION ( 'NONE',  ( 0.000000000000000000, 0.000000000000000000, 1.000000000000000000 ) ) ;
#51295=ORIENTED_EDGE ( 'NONE', *, *, #35831, .F. ) ;
#51315=DIRECTION ( 'NONE',  ( 0.000000000000000000, 0.000000000000000000, 1.000000000000000000 ) ) ;
#51335=AXIS2_PLACEMENT_3D ( 'NONE', #30591, #6772, #51045 ) ;
#51356=AXIS2_PLACEMENT_3D ( 'NONE', #42391, #51232, #6488 ) ;
#51387=VERTEX_POINT ( 'NONE', #42875 ) ;
#51405=CARTESIAN_POINT ( 'NONE',  ( -18.86606260230390220, 19.38381105532060289, 16.21999999999999886 ) ) ;
#51407=DIRECTION ( 'NONE',  ( -8.660081000000000658E-17, -2.123755000000000144E-17, -1.000000000000000000 ) ) ;
#51438=EDGE_CURVE ( 'NONE', #371, #47191, #21798, .T. ) ;
#51462=VERTEX_POINT ( 'NONE', #24979 ) ;
#51467=CARTESIAN_POINT ( 'NONE',  ( -18.86606260230360022, -50.61618894467959962, 11.34999999999999964 ) ) ;
#51468=LINE ( 'NONE', #27598, #48264 ) ;
#51505=AXIS2_PLACEMENT_3D ( 'NONE', #39592, #3696, #28030 ) ;
#51507=ORIENTED_EDGE ( 'NONE', *, *, #49923, .F. ) ;
#51512=EDGE_CURVE ( 'NONE', #11148, #49525, #10073, .T. ) ;
#51520=VERTEX_POINT ( 'NONE', #44149 ) ;
#51579=DIRECTION ( 'NONE',  ( 0.000000000000000000, -0.7071067811865492381, 0.7071067811865457964 ) ) ;
#51590=EDGE_CURVE ( 'NONE', #47254, #8577, #11763, .T. ) ;
#51605=DIRECTION ( 'NONE',  ( 0.000000000000000000, 0.000000000000000000, 1.000000000000000000 ) ) ;
#51682=CIRCLE ( 'NONE', #1474, 1.000000000000000888 ) ;
#51698=DIRECTION ( 'NONE',  ( 0.000000000000000000, 0.000000000000000000, -1.000000000000000000 ) ) ;
#51702=EDGE_CURVE ( 'NONE', #7519, #13595, #45710, .T. ) ;
#51742=ORIENTED_EDGE ( 'NONE', *, *, #30582, .T. ) ;
#51803=CARTESIAN_POINT ( 'NONE',  ( 36.13393739769620083, -15.61618894467929941, -18.58999999999999986 ) ) ;
#51823=CIRCLE ( 'NONE', #13375, 18.50000000000000000 ) ;
#51840=DIRECTION ( 'NONE',  ( 0.000000000000000000, 0.000000000000000000, 1.000000000000000000 ) ) ;
#51853=AXIS2_PLACEMENT_3D ( 'NONE', #17600, #50352, #49586 ) ;
#51861=EDGE_CURVE ( 'NONE', #27489, #42283, #21577, .T. ) ;
ENDSEC;
END-ISO-10303-21;
